ISO-10303-21;
HEADER;
FILE_DESCRIPTION (('STEP AP214'),
    '1' );
FILE_NAME ('hex flange bolt small_iso_ISO 4162 - M5 x 25 x 16-N.step',
    '2026-10-06T08:09:25',
    ( '' ),
    ( '' ),
    'SwSTEP 2.0',
    'SolidWorks 2021',
    '' );
FILE_SCHEMA (( 'AUTOMOTIVE_DESIGN' ));
ENDSEC;

DATA;
#6=VERTEX_POINT ( 'NONE', #15550 ) ;
#22=LINE ( 'NONE', #7190, #18522 ) ;
#24=DIRECTION ( 'NONE',  ( -5.551115123125782702E-16, -1.201780285297635172E-31, 1.000000000000000000 ) ) ;
#25=CARTESIAN_POINT ( 'NONE',  ( 0.3126073911696447549, -2.020725942163688504, 3.499999999999997780 ) ) ;
#54=CARTESIAN_POINT ( 'NONE',  ( 0.000000000000000000, 3.031088913245528982, -1.750000000000001554 ) ) ;
#93=VERTEX_POINT ( 'NONE', #8036 ) ;
#192=DIRECTION ( 'NONE',  ( 5.551115123125782702E-16, 1.201780285297635172E-31, -1.000000000000000000 ) ) ;
#200=ORIENTED_EDGE ( 'NONE', *, *, #2322, .T. ) ;
#209=CARTESIAN_POINT ( 'NONE',  ( 4.050823680195219545, 2.400527758044904925, 2.978030508226147344 ) ) ;
#272=VECTOR ( 'NONE', #10209, 1000.000000000000000 ) ;
#312=AXIS2_PLACEMENT_3D ( 'NONE', #15353, #22544, #11935 ) ;
#322=AXIS2_PLACEMENT_3D ( 'NONE', #17727, #17856, #12431 ) ;
#335=CARTESIAN_POINT ( 'NONE',  ( 0.3126073911696447549, 2.020725942163688504, 3.499999999999997780 ) ) ;
#363=ADVANCED_FACE ( 'NONE', ( #4339 ), #722, .F. ) ;
#367=CARTESIAN_POINT ( 'NONE',  ( 4.158921614371309694, -4.076055977742306879, 0.05993604794450200363 ) ) ;
#373=ORIENTED_EDGE ( 'NONE', *, *, #22479, .F. ) ;
#427=ORIENTED_EDGE ( 'NONE', *, *, #3964, .F. ) ;
#428=PLANE ( 'NONE',  #6939 ) ;
#451=ORIENTED_EDGE ( 'NONE', *, *, #16114, .F. ) ;
#470=CONICAL_SURFACE ( 'NONE', #11727, 2.054999999999999716, 0.7853981633974502774 ) ;
#505=CARTESIAN_POINT ( 'NONE',  ( 4.175813232069142344, -4.122719923832743660, 0.000000000000000000 ) ) ;
#520=CARTESIAN_POINT ( 'NONE',  ( -1.228174534879794922E-15, 2.686816014504568528, 2.346298152288371686 ) ) ;
#527=CARTESIAN_POINT ( 'NONE',  ( 0.1381419387119304232, -1.355287006778805647, -3.500000000000008882 ) ) ;
#556=CIRCLE ( 'NONE', #18561, 5.200000000000001066 ) ;
#560=DIRECTION ( 'NONE',  ( 1.000000000000000000, 4.440892098500626162E-16, -5.551115123125782702E-16 ) ) ;
#583=ORIENTED_EDGE ( 'NONE', *, *, #2070, .T. ) ;
#592=CARTESIAN_POINT ( 'NONE',  ( 4.086376042167607636, -4.082715877136866567, 0.07147133206917638537 ) ) ;
#644=FACE_OUTER_BOUND ( 'NONE', #16321, .T. ) ;
#650=DIRECTION ( 'NONE',  ( 0.000000000000000000, 0.000000000000000000, 1.000000000000000000 ) ) ;
#673=CARTESIAN_POINT ( 'NONE',  ( 4.175075985190096262, 4.120741555260244660, 0.000000000000000000 ) ) ;
#685=CARTESIAN_POINT ( 'NONE',  ( 0.1397371499201708889, 1.362866705336855722, 3.499999999999994227 ) ) ;
#710=CARTESIAN_POINT ( 'NONE',  ( 3.951447005078447372, 1.347150628109124115, -3.499999999999999112 ) ) ;
#722=PLANE ( 'NONE',  #20502 ) ;
#758=DIRECTION ( 'NONE',  ( 5.551115123125782702E-16, 1.201780285297635172E-31, -1.000000000000000000 ) ) ;
#759=PRODUCT_DEFINITION_FORMATION_WITH_SPECIFIED_SOURCE ( 'ANY', '', #8169, .NOT_KNOWN. ) ;
#774=VERTEX_POINT ( 'NONE', #1977 ) ;
#784=CARTESIAN_POINT ( 'NONE',  ( 5.599999999999994316, -4.041451884327383226, 0.000000000000000000 ) ) ;
#825=CARTESIAN_POINT ( 'NONE',  ( 4.175075985190096262, 2.060370777630125882, -3.568666869285561649 ) ) ;
#875=FACE_OUTER_BOUND ( 'NONE', #22915, .T. ) ;
#878=CARTESIAN_POINT ( 'NONE',  ( -1.276902167985857367E-15, -2.859595677584336748, 2.047034997319572280 ) ) ;
#920=( LENGTH_UNIT ( ) NAMED_UNIT ( * ) SI_UNIT ( .MILLI., .METRE. ) );
#933=ORIENTED_EDGE ( 'NONE', *, *, #1286, .T. ) ;
#986=ORIENTED_EDGE ( 'NONE', *, *, #3342, .F. ) ;
#995=CARTESIAN_POINT ( 'NONE',  ( 4.033906725095055990, -1.419670120618832465, 3.499999999999995559 ) ) ;
#998=DIRECTION ( 'NONE',  ( -1.000000000000000000, -4.440892098500626162E-16, 5.551115123125782702E-16 ) ) ;
#1012=CARTESIAN_POINT ( 'NONE',  ( 4.071447262713884463, 2.020725942163688504, -3.499999999999999556 ) ) ;
#1025=EDGE_CURVE ( 'NONE', #18414, #9641, #4374, .T. ) ;
#1031=EDGE_LOOP ( 'NONE', ( #7562, #11286, #14290 ) ) ;
#1033=CARTESIAN_POINT ( 'NONE',  ( 4.033901012037268252, 2.321269032827638856, 2.979444097106773270 ) ) ;
#1047=B_SPLINE_CURVE_WITH_KNOTS ( 'NONE', 3,
 ( #15162, #21881, #12942, #825, #4215, #3990, #9762, #11397, #7876, #2578, #2110, #13057, #7994, #15038, #22231, #11171 ),
 .UNSPECIFIED., .F., .F.,
 ( 4, 3, 3, 3, 3, 4 ),
 ( -2.111273352577022893E-06, 0.000000000000000000, 3.519286887793240313E-05, 7.191842652067673993E-05, 0.0001049868727093628386, 0.0001382836236822181791 ),
 .UNSPECIFIED. ) ;
#1063=VECTOR ( 'NONE', #6055, 1000.000000000000000 ) ;
#1119=CARTESIAN_POINT ( 'NONE',  ( 0.2174200650117549538, -2.185595227304856447, 3.214438021527930456 ) ) ;
#1141=CARTESIAN_POINT ( 'NONE',  ( 4.630153689607049650, 0.000000000000000000, 0.000000000000000000 ) ) ;
#1150=CARTESIAN_POINT ( 'NONE',  ( 4.158921614371306141, 4.076055977742309544, -0.05993604794450450857 ) ) ;
#1158=CARTESIAN_POINT ( 'NONE',  ( 0.000000000000000000, 0.000000000000000000, 0.000000000000000000 ) ) ;
#1167=DIRECTION ( 'NONE',  ( -1.000000000000000000, -4.440892098500626162E-16, 5.551115123125782702E-16 ) ) ;
#1200=CARTESIAN_POINT ( 'NONE',  ( 4.170895651974849905, -4.109780709045216973, 1.853155041415897988E-14 ) ) ;
#1203=AXIS2_PLACEMENT_3D ( 'NONE', #1141, #1478, #8650 ) ;
#1214=ADVANCED_FACE ( 'NONE', ( #5498 ), #14910, .F. ) ;
#1221=CARTESIAN_POINT ( 'NONE',  ( 4.175813232069142344, -2.061359961916371830, -3.570380186727398986 ) ) ;
#1227=CARTESIAN_POINT ( 'NONE',  ( 4.630153689607049650, 0.000000000000000000, 0.000000000000000000 ) ) ;
#1232=CARTESIAN_POINT ( 'NONE',  ( 3.878096787214414753, -2.680238624820921345, 2.357690525401619830 ) ) ;
#1246=CARTESIAN_POINT ( 'NONE',  ( 5.599999999999994316, 0.000000000000000000, 0.000000000000000000 ) ) ;
#1272=CARTESIAN_POINT ( 'NONE',  ( 4.165266963751715679, 2.049631966911993786, 3.550066703508900634 ) ) ;
#1280=CARTESIAN_POINT ( 'NONE',  ( 3.951447005078446484, -3.704664227300101143, 0.5833333333333329263 ) ) ;
#1284=B_SPLINE_CURVE_WITH_KNOTS ( 'NONE', 3,
 ( #1652, #6958, #21305, #12340, #20109, #21655 ),
 .UNSPECIFIED., .F., .F.,
 ( 4, 2, 4 ),
 ( 0.01103795673506155310, 0.01206113197427182565, 0.01308430721348209647 ),
 .UNSPECIFIED. ) ;
#1286=EDGE_CURVE ( 'NONE', #6388, #774, #23033, .T. ) ;
#1328=UNCERTAINTY_MEASURE_WITH_UNIT (LENGTH_MEASURE( 1.000000000000000082E-05 ), #920, 'distance_accuracy_value', 'NONE');
#1343=CARTESIAN_POINT ( 'NONE',  ( 4.158806752148102248, -2.089318365061878069, 3.499999999999995115 ) ) ;
#1357=ORIENTED_EDGE ( 'NONE', *, *, #4323, .T. ) ;
#1368=LINE ( 'NONE', #3251, #10465 ) ;
#1380=CARTESIAN_POINT ( 'NONE',  ( 4.052424581287492167, 3.786734753434579215, 0.5771415817955150018 ) ) ;
#1385=CARTESIAN_POINT ( 'NONE',  ( 4.175075985190096262, 2.060370777630112116, 3.568666869285570531 ) ) ;
#1393=CARTESIAN_POINT ( 'NONE',  ( 0.000000000000000000, 0.000000000000000000, 0.000000000000000000 ) ) ;
#1431=ORIENTED_EDGE ( 'NONE', *, *, #2761, .T. ) ;
#1452=CARTESIAN_POINT ( 'NONE',  ( 0.000000000000000000, 3.031088913245528982, -1.750000000000001554 ) ) ;
#1477=B_SPLINE_CURVE_WITH_KNOTS ( 'NONE', 3,
 ( #3275, #1280, #2918, #21039, #3037 ),
 .UNSPECIFIED., .F., .F.,
 ( 4, 1, 4 ),
 ( 0.000000000000000000, 0.002020725942163690073, 0.004041451884327380145 ),
 .UNSPECIFIED. ) ;
#1478=DIRECTION ( 'NONE',  ( 1.000000000000000000, 4.440892098500626162E-16, -5.551115123125782702E-16 ) ) ;
#1489=CARTESIAN_POINT ( 'NONE',  ( 3.973514160553464514, 3.435084588004195805, -1.181876024140321224 ) ) ;
#1580=LINE ( 'NONE', #10636, #7257 ) ;
#1651=CARTESIAN_POINT ( 'NONE',  ( 4.071447262713884463, -2.020725942163695166, -3.500000000000000444 ) ) ;
#1652=CARTESIAN_POINT ( 'NONE',  ( 0.3126073911696447549, 2.020725942163688504, -3.499999999999996003 ) ) ;
#1679=AXIS2_PLACEMENT_3D ( 'NONE', #13346, #7927, #22169 ) ;
#1696=EDGE_LOOP ( 'NONE', ( #4486, #11895, #583, #986, #20627 ) ) ;
#1698=ORIENTED_EDGE ( 'NONE', *, *, #1286, .F. ) ;
#1807=ORIENTED_EDGE ( 'NONE', *, *, #17435, .T. ) ;
#1808=CIRCLE ( 'NONE', #10459, 2.054999999999999716 ) ;
#1832=ORIENTED_EDGE ( 'NONE', *, *, #4323, .F. ) ;
#1835=( GEOMETRIC_REPRESENTATION_CONTEXT ( 3 ) GLOBAL_UNCERTAINTY_ASSIGNED_CONTEXT ( ( #19192 ) ) GLOBAL_UNIT_ASSIGNED_CONTEXT ( ( #12532, #5487, #10539 ) ) REPRESENTATION_CONTEXT ( 'NONE', 'WORKASPACE' ) );
#1859=ORIENTED_EDGE ( 'NONE', *, *, #20481, .T. ) ;
#1870=CARTESIAN_POINT ( 'NONE',  ( 5.599999999999991651, 6.539831464966449098E-16, -5.200000000000001066 ) ) ;
#1893=( BOUNDED_SURFACE ( )  B_SPLINE_SURFACE ( 3, 2, ( 
 ( #2460, #11282, #7534 ),
 ( #18354, #18464, #20243 ),
 ( #9296, #5774, #6118 ),
 ( #18586, #9418, #16915 ),
 ( #16455, #13176, #4330 ),
 ( #592, #367, #7757 ) ),
 .UNSPECIFIED., .F., .F., .T. ) 
 B_SPLINE_SURFACE_WITH_KNOTS ( ( 4, 2, 4 ),
 ( 3, 3 ),
 ( 0.01651999345535505245, 0.01858032176739834312, 0.02064065007944163727 ),
 ( 0.000000000000000000, 1.000000000000000000 ),
 .UNSPECIFIED. ) 
 GEOMETRIC_REPRESENTATION_ITEM ( )  RATIONAL_B_SPLINE_SURFACE ( (
 ( 1.000000000000000000, 0.8047781103519393575, 1.000000000000000000),
 ( 1.000000000000000000, 0.8123785825603665467, 1.000000000000000000),
 ( 1.000000000000000000, 0.8190671539789206035, 1.000000000000000000),
 ( 1.000000000000000000, 0.8192352254833937808, 1.000000000000000000),
 ( 1.000000000000000000, 0.8126129677212307056, 1.000000000000000000),
 ( 1.000000000000000000, 0.8047712537969730073, 1.000000000000000000) ) ) 
 REPRESENTATION_ITEM ( '' )  SURFACE ( )  );
#1917=CARTESIAN_POINT ( 'NONE',  ( 4.093692494532772841, 2.021783646005771207, 3.501831996793840052 ) ) ;
#1932=EDGE_CURVE ( 'NONE', #20684, #7007, #22440, .T. ) ;
#1977=CARTESIAN_POINT ( 'NONE',  ( 0.3126073911695753660, -2.020725942163792421, -3.499999999999996891 ) ) ;
#1981=SURFACE_STYLE_FILL_AREA ( #19761 ) ;
#1984=CARTESIAN_POINT ( 'NONE',  ( 3.951447005078449148, -3.704664227300103807, -0.5833333333333333703 ) ) ;
#2023=CARTESIAN_POINT ( 'NONE',  ( 3.972709601346594344, -2.746729940827189687, 2.374099244652733365 ) ) ;
#2056=PRODUCT_DEFINITION_CONTEXT ( 'detailed design', #17494, 'design' ) ;
#2070=EDGE_CURVE ( 'NONE', #7007, #10462, #19988, .T. ) ;
#2074=CARTESIAN_POINT ( 'NONE',  ( 5.599999999999991651, -6.249257483547704998E-31, 5.200000000000001066 ) ) ;
#2110=CARTESIAN_POINT ( 'NONE',  ( 4.124214193018072905, 2.028338413290942110, -3.513185186763557066 ) ) ;
#2137=CARTESIAN_POINT ( 'NONE',  ( 2.591920818598158051E-16, 2.859595677584346074, -2.047034997319578498 ) ) ;
#2176=ORIENTED_EDGE ( 'NONE', *, *, #23022, .F. ) ;
#2177=CIRCLE ( 'NONE', #7459, 5.371010071662833063 ) ;
#2239=EDGE_CURVE ( 'NONE', #4523, #4400, #2177, .T. ) ;
#2259=CARTESIAN_POINT ( 'NONE',  ( 0.02993401039713806250, 2.688325911136462132, -2.343682934607768331 ) ) ;
#2322=EDGE_CURVE ( 'NONE', #17450, #4649, #1808, .T. ) ;
#2326=DIRECTION ( 'NONE',  ( -1.000000000000000000, -4.440892098500626162E-16, 5.551115123125782702E-16 ) ) ;
#2341=CARTESIAN_POINT ( 'NONE',  ( 3.806834918298642290, -9.107298248878237246E-15, -3.500000000000012434 ) ) ;
#2343=CIRCLE ( 'NONE', #13978, 5.371010071662833063 ) ;
#2349=EDGE_CURVE ( 'NONE', #93, #10626, #10824, .T. ) ;
#2350=AXIS2_PLACEMENT_3D ( 'NONE', #1158, #2800, #11849 ) ;
#2361=CARTESIAN_POINT ( 'NONE',  ( 4.132952817037863547, -2.031684012687259955, 3.518979934899748141 ) ) ;
#2371=CARTESIAN_POINT ( 'NONE',  ( 4.630153689607052314, 6.577590292450120328E-16, 5.371010071662848162 ) ) ;
#2373=CARTESIAN_POINT ( 'NONE',  ( 4.175813232069142344, 2.061359961916371830, 3.570380186727395433 ) ) ;
#2391=AXIS2_PLACEMENT_3D ( 'NONE', #5990, #2326, #19981 ) ;
#2399=DIRECTION ( 'NONE',  ( -5.551115123125782702E-16, -1.201780285297635172E-31, 1.000000000000000000 ) ) ;
#2410=ORIENTED_EDGE ( 'NONE', *, *, #2903, .T. ) ;
#2413=ORIENTED_EDGE ( 'NONE', *, *, #7152, .F. ) ;
#2420=PLANE ( 'NONE',  #10240 ) ;
#2426=CARTESIAN_POINT ( 'NONE',  ( 4.132952817037863547, 4.063368025374527015, 0.000000000000000000 ) ) ;
#2460=CARTESIAN_POINT ( 'NONE',  ( 4.086262629614027198, -1.979770830881093513, -3.570936333571106847 ) ) ;
#2476=CARTESIAN_POINT ( 'NONE',  ( 4.104070371397483541, -2.023683613428369110, 3.505122836902506922 ) ) ;
#2483=ADVANCED_FACE ( 'NONE', ( #16758 ), #16106, .T. ) ;
#2500=VERTEX_POINT ( 'NONE', #2074 ) ;
#2507=DIRECTION ( 'NONE',  ( 1.000000000000000000, 4.440892098500626162E-16, -5.551115123125782702E-16 ) ) ;
#2560=VERTEX_POINT ( 'NONE', #13020 ) ;
#2578=CARTESIAN_POINT ( 'NONE',  ( 4.132952817037863547, 2.031684012687259955, -3.518979934899751694 ) ) ;
#2594=CARTESIAN_POINT ( 'NONE',  ( 30.60000000000000142, 2.775557561562891351E-14, 2.054999999999978844 ) ) ;
#2619=DIRECTION ( 'NONE',  ( -1.000000000000000000, -4.440892098500626162E-16, 5.551115123125782702E-16 ) ) ;
#2666=FACE_OUTER_BOUND ( 'NONE', #8055, .T. ) ;
#2695=ORIENTED_EDGE ( 'NONE', *, *, #1025, .F. ) ;
#2731=ORIENTED_EDGE ( 'NONE', *, *, #16144, .F. ) ;
#2744=CARTESIAN_POINT ( 'NONE',  ( 3.974183935050618732, -0.7239581970533588429, 3.565826011443267163 ) ) ;
#2746=FACE_OUTER_BOUND ( 'NONE', #13879, .T. ) ;
#2750=CARTESIAN_POINT ( 'NONE',  ( 4.030859730899970295, -1.403482646611178053, -3.500000000000007105 ) ) ;
#2751=ORIENTED_EDGE ( 'NONE', *, *, #8398, .F. ) ;
#2753=EDGE_CURVE ( 'NONE', #20007, #4400, #20598, .T. ) ;
#2755=AXIS2_PLACEMENT_3D ( 'NONE', #8649, #17468, #6768 ) ;
#2757=ORIENTED_EDGE ( 'NONE', *, *, #4488, .F. ) ;
#2761=EDGE_CURVE ( 'NONE', #9641, #18414, #22476, .T. ) ;
#2780=CARTESIAN_POINT ( 'NONE',  ( 4.170895651974849905, 4.109780709045216973, 2.320551093086091258E-18 ) ) ;
#2794=EDGE_LOOP ( 'NONE', ( #16780, #451, #4051, #2757 ) ) ;
#2800=DIRECTION ( 'NONE',  ( 1.000000000000000000, 4.440892098500626162E-16, -5.551115123125782702E-16 ) ) ;
#2818=CARTESIAN_POINT ( 'NONE',  ( 5.599999999999994316, 2.020725942163688504, 3.499999999999997780 ) ) ;
#2836=CARTESIAN_POINT ( 'NONE',  ( 4.050823680195218657, -2.400527758044904036, -2.978030508226148676 ) ) ;
#2870=FACE_OUTER_BOUND ( 'NONE', #13873, .T. ) ;
#2876=AXIS2_PLACEMENT_3D ( 'NONE', #6450, #9751, #22799 ) ;
#2884=ORIENTED_EDGE ( 'NONE', *, *, #16144, .T. ) ;
#2901=CARTESIAN_POINT ( 'NONE',  ( 3.961551342854980451, 2.319461885623427477, 2.982574167880718274 ) ) ;
#2903=EDGE_CURVE ( 'NONE', #17297, #5230, #1368, .T. ) ;
#2918=CARTESIAN_POINT ( 'NONE',  ( 3.806834918298643178, -3.031088913245532979, 1.749999999999997113 ) ) ;
#2963=DIRECTION ( 'NONE',  ( 0.000000000000000000, 0.000000000000000000, 1.000000000000000000 ) ) ;
#2999=ORIENTED_EDGE ( 'NONE', *, *, #16197, .T. ) ;
#3031=CARTESIAN_POINT ( 'NONE',  ( 4.151274195509674136, 2.039912954708746007, 3.533232880573493162 ) ) ;
#3037=CARTESIAN_POINT ( 'NONE',  ( 4.071447262713884463, -2.020725942163688504, 3.499999999999997780 ) ) ;
#3040=DIRECTION ( 'NONE',  ( -4.844685039213900252E-16, -1.201780285297635172E-31, 1.000000000000000000 ) ) ;
#3045=CARTESIAN_POINT ( 'NONE',  ( -1.418636431716181459E-15, -3.375361811986499205, 1.153701847711630091 ) ) ;
#3075=CARTESIAN_POINT ( 'NONE',  ( 4.071447262713884463, -4.041451884327383226, 0.000000000000000000 ) ) ;
#3131=DIRECTION ( 'NONE',  ( -1.000000000000000000, -4.440892098500626162E-16, 5.551115123125782702E-16 ) ) ;
#3146=CARTESIAN_POINT ( 'NONE',  ( 3.880206590543184841, 2.665671387532550174, 2.382921720511005592 ) ) ;
#3152=B_SPLINE_CURVE_WITH_KNOTS ( 'NONE', 3,
 ( #4228, #11187, #20362, #2476, #5678, #22245, #2361, #15053, #9550, #16473, #20492, #9655, #7892, #6133, #9199, #13312 ),
 .UNSPECIFIED., .F., .F.,
 ( 4, 3, 3, 3, 3, 4 ),
 ( 0.000000000000000000, 3.315506744709602110E-05, 6.608280158699783688E-05, 0.0001026520855291450108, 0.0001376952025664789059, 0.0001398064759190598540 ),
 .UNSPECIFIED. ) ;
#3154=CARTESIAN_POINT ( 'NONE',  ( 4.114405500665259119, 2.025575754679715068, 3.508400121684933204 ) ) ;
#3202=CARTESIAN_POINT ( 'NONE',  ( 4.142654963991858175, -4.070796997468697498, -4.252513780320472990E-18 ) ) ;
#3251=CARTESIAN_POINT ( 'NONE',  ( 5.599999999999994316, 4.041451884327383226, 0.000000000000000000 ) ) ;
#3262=CARTESIAN_POINT ( 'NONE',  ( 4.050823680195218657, 3.779313952391380571, -0.5899027668435183891 ) ) ;
#3275=CARTESIAN_POINT ( 'NONE',  ( 4.071447262713884463, -4.041451884327383226, 0.000000000000000000 ) ) ;
#3284=DIRECTION ( 'NONE',  ( 1.000000000000000000, 4.440892098500626162E-16, -5.551115123125782702E-16 ) ) ;
#3289=DIRECTION ( 'NONE',  ( 5.551115123125782702E-16, 3.966469614587832056E-31, 1.000000000000000000 ) ) ;
#3306=CARTESIAN_POINT ( 'NONE',  ( 3.806834918298646731, -3.031088913245542749, -1.750000000000002887 ) ) ;
#3342=EDGE_CURVE ( 'NONE', #11851, #10462, #21836, .T. ) ;
#3353=EDGE_LOOP ( 'NONE', ( #11315, #3942, #1859 ) ) ;
#3383=AXIS2_PLACEMENT_3D ( 'NONE', #17279, #19525, #6473 ) ;
#3405=FACE_OUTER_BOUND ( 'NONE', #18244, .T. ) ;
#3411=ORIENTED_EDGE ( 'NONE', *, *, #22441, .F. ) ;
#3428=CARTESIAN_POINT ( 'NONE',  ( 4.093692494532772841, -4.043567292011542413, 5.760878920963493723E-18 ) ) ;
#3490=EDGE_CURVE ( 'NONE', #10462, #12775, #12820, .T. ) ;
#3511=CARTESIAN_POINT ( 'NONE',  ( 0.000000000000000000, 0.000000000000000000, 0.000000000000000000 ) ) ;
#3574=CARTESIAN_POINT ( 'NONE',  ( 3.880206590543184841, -3.396506438958554863, 1.117078279488939785 ) ) ;
#3580=VERTEX_POINT ( 'NONE', #12316 ) ;
#3637=ORIENTED_EDGE ( 'NONE', *, *, #3342, .T. ) ;
#3685=ORIENTED_EDGE ( 'NONE', *, *, #12395, .F. ) ;
#3711=VECTOR ( 'NONE', #20089, 1000.000000000000000 ) ;
#3728=( GEOMETRIC_REPRESENTATION_CONTEXT ( 3 ) GLOBAL_UNCERTAINTY_ASSIGNED_CONTEXT ( ( #4363 ) ) GLOBAL_UNIT_ASSIGNED_CONTEXT ( ( #14466, #7067, #15977 ) ) REPRESENTATION_CONTEXT ( 'NONE', 'WORKASPACE' ) );
#3740=EDGE_CURVE ( 'NONE', #9641, #93, #4077, .T. ) ;
#3746=PRESENTATION_STYLE_ASSIGNMENT (( #5292 ) ) ;
#3783=FACE_OUTER_BOUND ( 'NONE', #22504, .T. ) ;
#3790=CARTESIAN_POINT ( 'NONE',  ( 0.3126073911696447549, 4.041451884327383226, 0.000000000000000000 ) ) ;
#3830=CARTESIAN_POINT ( 'NONE',  ( 4.175813232069142344, -2.061359961916371830, -3.570380186727398986 ) ) ;
#3901=CARTESIAN_POINT ( 'NONE',  ( 4.050536630291682982, -2.401306687817042818, 2.976670123173756899 ) ) ;
#3942=ORIENTED_EDGE ( 'NONE', *, *, #14570, .T. ) ;
#3964=EDGE_CURVE ( 'NONE', #11851, #6388, #10519, .T. ) ;
#3990=CARTESIAN_POINT ( 'NONE',  ( 4.165266963751725449, 2.049631966911992453, -3.550066703508908184 ) ) ;
#4020=ORIENTED_EDGE ( 'NONE', *, *, #12395, .T. ) ;
#4032=FACE_OUTER_BOUND ( 'NONE', #10632, .T. ) ;
#4045=PLANE ( 'NONE',  #1679 ) ;
#4051=ORIENTED_EDGE ( 'NONE', *, *, #19935, .F. ) ;
#4077=LINE ( 'NONE', #11254, #3711 ) ;
#4082=EDGE_CURVE ( 'NONE', #10053, #20034, #5945, .T. ) ;
#4091=B_SPLINE_CURVE_WITH_KNOTS ( 'NONE', 3,
 ( #15178, #22371, #6253, #5032, #2836, #20606 ),
 .UNSPECIFIED., .F., .F.,
 ( 4, 2, 4 ),
 ( 0.000000000000000000, 0.002086519881787258883, 0.004173039763574517766 ),
 .UNSPECIFIED. ) ;
#4106=CARTESIAN_POINT ( 'NONE',  ( 0.000000000000000000, 0.000000000000000000, 0.000000000000000000 ) ) ;
#4113=DIRECTION ( 'NONE',  ( -1.000000000000000000, -4.440892098500626162E-16, 5.551115123125782702E-16 ) ) ;
#4171=AXIS2_PLACEMENT_3D ( 'NONE', #10760, #13080, #14952 ) ;
#4190=ORIENTED_EDGE ( 'NONE', *, *, #2761, .F. ) ;
#4215=CARTESIAN_POINT ( 'NONE',  ( 4.170895651974850793, 2.054890354522583618, -3.559174498016392185 ) ) ;
#4223=CARTESIAN_POINT ( 'NONE',  ( 0.000000000000000000, 0.000000000000000000, 0.000000000000000000 ) ) ;
#4228=CARTESIAN_POINT ( 'NONE',  ( 4.071447262713884463, -2.020725942163688504, 3.499999999999997780 ) ) ;
#4297=SHAPE_REPRESENTATION ( 'hex flange bolt small_iso_ISO 4162 - M5 x 25 x 16-N', ( #22115 ), #17228 ) ;
#4306=EDGE_CURVE ( 'NONE', #12775, #20034, #6104, .T. ) ;
#4323=EDGE_CURVE ( 'NONE', #18414, #10626, #16965, .T. ) ;
#4328=CARTESIAN_POINT ( 'NONE',  ( 4.071447262713884463, -2.020725942163695166, -3.500000000000000444 ) ) ;
#4330=CARTESIAN_POINT ( 'NONE',  ( 4.052424581287676908, -3.786734753435080147, -0.5771415817957217254 ) ) ;
#4339=FACE_OUTER_BOUND ( 'NONE', #9594, .T. ) ;
#4363=UNCERTAINTY_MEASURE_WITH_UNIT (LENGTH_MEASURE( 1.000000000000000082E-05 ), #14466, 'distance_accuracy_value', 'NONE');
#4374=CIRCLE ( 'NONE', #2876, 2.500000000000002220 ) ;
#4377=CARTESIAN_POINT ( 'NONE',  ( 5.599999999999994316, 2.020725942163688504, -3.500000000000005773 ) ) ;
#4389=CARTESIAN_POINT ( 'NONE',  ( 4.180232103119974063, 2.085387772176683807, -3.570466442734705481 ) ) ;
#4400=VERTEX_POINT ( 'NONE', #6865 ) ;
#4418=CARTESIAN_POINT ( 'NONE',  ( 0.000000000000000000, 3.031088913245536087, 1.750000000000003331 ) ) ;
#4425=CARTESIAN_POINT ( 'NONE',  ( 4.180231891692618440, 2.049421325483208545, 3.591231015387279957 ) ) ;
#4486=ORIENTED_EDGE ( 'NONE', *, *, #10023, .F. ) ;
#4488=EDGE_CURVE ( 'NONE', #17187, #5552, #23198, .T. ) ;
#4517=CARTESIAN_POINT ( 'NONE',  ( 4.086375874528098251, -2.103253014742891391, -3.500000000000007105 ) ) ;
#4521=ORIENTED_EDGE ( 'NONE', *, *, #1932, .F. ) ;
#4523=VERTEX_POINT ( 'NONE', #2371 ) ;
#4525=ORIENTED_EDGE ( 'NONE', *, *, #17435, .F. ) ;
#4530=ORIENTED_EDGE ( 'NONE', *, *, #16463, .F. ) ;
#4537=CARTESIAN_POINT ( 'NONE',  ( 4.158413352280815545, 4.089743253945648860, -1.734723475976807094E-15 ) ) ;
#4628=CARTESIAN_POINT ( 'NONE',  ( 3.950233766685598447, 0.7256672287173716596, -3.500000000000161204 ) ) ;
#4646=CARTESIAN_POINT ( 'NONE',  ( 3.806834918298639625, 3.031088913245540528, -1.750000000000002442 ) ) ;
#4649=VERTEX_POINT ( 'NONE', #2594 ) ;
#4687=B_SPLINE_CURVE_WITH_KNOTS ( 'NONE', 3,
 ( #5587, #17485, #1917, #5017, #3154, #21150, #14512, #10317, #3031, #21700, #1272, #10195, #1385, #9102, #12747, #8448 ),
 .UNSPECIFIED., .F., .F.,
 ( 4, 3, 3, 3, 3, 4 ),
 ( 0.000000000000000000, 3.315506744709155554E-05, 6.608280158698813327E-05, 0.0001026520855291343043, 0.0001376952025664795565, 0.0001398064759190610737 ),
 .UNSPECIFIED. ) ;
#4713=EDGE_CURVE ( 'NONE', #5552, #18229, #4091, .T. ) ;
#4747=CARTESIAN_POINT ( 'NONE',  ( 3.878104551856317972, -0.7018542299754928493, -3.500000000000006661 ) ) ;
#4834=CARTESIAN_POINT ( 'NONE',  ( 4.124214193018073793, -4.056676826581885997, 3.830195444513743874E-18 ) ) ;
#4843=EDGE_LOOP ( 'NONE', ( #11634, #12390, #14016, #4525 ) ) ;
#4853=COLOUR_RGB ( '', 0.72549020, 0.75294118, 0.79215686) ;
#4859=CARTESIAN_POINT ( 'NONE',  ( 4.052424581287934480, -2.393186648133822203, 2.990837702970649215 ) ) ;
#4876=CARTESIAN_POINT ( 'NONE',  ( 30.15500000000000114, 2.775557561562891351E-14, -2.081668171172168513E-14 ) ) ;
#4888=CARTESIAN_POINT ( 'NONE',  ( 3.948103430091018939, 3.379418997638859778, 1.146674596026393100 ) ) ;
#4937=EDGE_CURVE ( 'NONE', #17297, #9451, #15041, .T. ) ;
#4943=CARTESIAN_POINT ( 'NONE',  ( 0.000000000000000000, 0.000000000000000000, 0.000000000000000000 ) ) ;
#4966=CARTESIAN_POINT ( 'NONE',  ( 3.880214671983731822, -0.7309020039786242595, 3.499999999999996003 ) ) ;
#4994=CARTESIAN_POINT ( 'NONE',  ( 3.973110223765529803, 0.6902454861566474920, -3.565797985667399139 ) ) ;
#5008=SURFACE_STYLE_FILL_AREA ( #8782 ) ;
#5017=CARTESIAN_POINT ( 'NONE',  ( 4.104070371397483541, 2.023683613428369110, 3.505122836902505146 ) ) ;
#5032=CARTESIAN_POINT ( 'NONE',  ( 3.973514160553465402, -2.741076955031368279, -2.383932505289874548 ) ) ;
#5095=CARTESIAN_POINT ( 'NONE',  ( 3.948095570617040639, 0.6965071952230758034, 3.499999999999995559 ) ) ;
#5129=FILL_AREA_STYLE_COLOUR ( '', #19884 ) ;
#5130=CARTESIAN_POINT ( 'NONE',  ( 4.175813232069142344, 4.122719923832743660, 0.000000000000000000 ) ) ;
#5178=CARTESIAN_POINT ( 'NONE',  ( 3.951447005078446484, -2.357513599190976805, -2.916666666666666963 ) ) ;
#5213=ADVANCED_FACE ( 'NONE', ( #2746 ), #4045, .F. ) ;
#5230=VERTEX_POINT ( 'NONE', #6053 ) ;
#5246=DIRECTION ( 'NONE',  ( -1.000000000000000000, -4.440892098500626162E-16, 5.551115123125782702E-16 ) ) ;
#5251=ADVANCED_FACE ( 'NONE', ( #9932 ), #470, .T. ) ;
#5257=( NAMED_UNIT ( * ) SI_UNIT ( $, .STERADIAN. ) SOLID_ANGLE_UNIT ( ) );
#5268=CARTESIAN_POINT ( 'NONE',  ( 3.878096787214412089, 2.680238624820988402, -2.357690525401514137 ) ) ;
#5292=SURFACE_STYLE_USAGE ( .BOTH. , #16093 ) ;
#5306=DIRECTION ( 'NONE',  ( 1.000000000000000000, 0.000000000000000000, 0.000000000000000000 ) ) ;
#5351=EDGE_CURVE ( 'NONE', #10626, #93, #7976, .T. ) ;
#5386=EDGE_CURVE ( 'NONE', #4400, #4523, #2343, .T. ) ;
#5388=CARTESIAN_POINT ( 'NONE',  ( 3.972066048304740971, 2.740530939476234717, -2.384802634787816178 ) ) ;
#5404=DIRECTION ( 'NONE',  ( -1.000000000000000000, -4.440892098500626162E-16, 5.551115123125782702E-16 ) ) ;
#5432=CARTESIAN_POINT ( 'NONE',  ( 4.071447262713884463, -4.041451884327383226, 0.000000000000000000 ) ) ;
#5487=( NAMED_UNIT ( * ) PLANE_ANGLE_UNIT ( ) SI_UNIT ( $, .RADIAN. ) );
#5498=FACE_OUTER_BOUND ( 'NONE', #20907, .T. ) ;
#5499=CARTESIAN_POINT ( 'NONE',  ( 4.142654963991857286, -2.035398498734348305, -3.525413613457310635 ) ) ;
#5502=DIRECTION ( 'NONE',  ( -1.000000000000000000, -4.440892098500626162E-16, 5.551115123125782702E-16 ) ) ;
#5523=ADVANCED_FACE ( 'NONE', ( #3783 ), #10604, .T. ) ;
#5552=VERTEX_POINT ( 'NONE', #11422 ) ;
#5587=CARTESIAN_POINT ( 'NONE',  ( 4.071447262713884463, 2.020725942163688504, 3.499999999999997780 ) ) ;
#5596=B_SPLINE_CURVE_WITH_KNOTS ( 'NONE', 3,
 ( #22229, #710, #2341, #21773, #4328 ),
 .UNSPECIFIED., .F., .F.,
 ( 4, 1, 4 ),
 ( 0.000000000000000000, 0.002020725942163693108, 0.004041451884327386217 ),
 .UNSPECIFIED. ) ;
#5653=DIRECTION ( 'NONE',  ( 4.440892098500626162E-16, -1.000000000000000000, 1.263410043518026720E-31 ) ) ;
#5678=CARTESIAN_POINT ( 'NONE',  ( 4.114405500665259119, -2.025575754679715512, 3.508400121684935424 ) ) ;
#5695=B_SPLINE_CURVE_WITH_KNOTS ( 'NONE', 3,
 ( #7490, #7039, #9027, #14211, #209, #21732 ),
 .UNSPECIFIED., .F., .F.,
 ( 4, 2, 4 ),
 ( 0.000000000000000000, 0.002086519881787257148, 0.004173039763574514296 ),
 .UNSPECIFIED. ) ;
#5696=ORIENTED_EDGE ( 'NONE', *, *, #8398, .T. ) ;
#5732=CARTESIAN_POINT ( 'NONE',  ( 4.093692494532772841, -2.021783646005771207, -3.501831996793843604 ) ) ;
#5774=CARTESIAN_POINT ( 'NONE',  ( 3.950241966888154099, -2.668221755853662724, -2.378504353000910676 ) ) ;
#5808=CARTESIAN_POINT ( 'NONE',  ( 4.050823680195218657, -3.779313952391380571, 0.5899027668435161686 ) ) ;
#5811=CARTESIAN_POINT ( 'NONE',  ( 5.775087817974630717E-16, 3.375361811986508975, -1.153701847711636086 ) ) ;
#5821=ORIENTED_EDGE ( 'NONE', *, *, #16114, .T. ) ;
#5838=CARTESIAN_POINT ( 'NONE',  ( 0.000000000000000000, 0.000000000000000000, 0.000000000000000000 ) ) ;
#5945=LINE ( 'NONE', #14645, #1063 ) ;
#5971=CARTESIAN_POINT ( 'NONE',  ( 4.165266963751727225, 4.099263933823985795, -1.987707336973076212E-15 ) ) ;
#5987=EDGE_LOOP ( 'NONE', ( #7706, #8026, #19573, #1832 ) ) ;
#5990=CARTESIAN_POINT ( 'NONE',  ( 5.599999999999994316, 0.000000000000000000, 0.000000000000000000 ) ) ;
#6032=EDGE_CURVE ( 'NONE', #8438, #20684, #5596, .T. ) ;
#6053=CARTESIAN_POINT ( 'NONE',  ( 0.3126073911696447549, 4.041451884327383226, 0.000000000000000000 ) ) ;
#6055=DIRECTION ( 'NONE',  ( -1.000000000000000000, -4.440892098500626162E-16, 5.551115123125782702E-16 ) ) ;
#6057=DIRECTION ( 'NONE',  ( 1.000000000000000000, 4.440892098500626162E-16, 5.551115123125782702E-16 ) ) ;
#6083=CARTESIAN_POINT ( 'NONE',  ( 0.02993401039713629655, 3.373851915354614928, 1.156317065392238774 ) ) ;
#6092=VERTEX_POINT ( 'NONE', #15386 ) ;
#6104=B_SPLINE_CURVE_WITH_KNOTS ( 'NONE', 3,
 ( #20762, #878, #6627, #8164, #1119, #17441 ),
 .UNSPECIFIED., .F., .F.,
 ( 4, 2, 4 ),
 ( 0.002044882221487533212, 0.003063384235218495448, 0.004081886248949457251 ),
 .UNSPECIFIED. ) ;
#6118=CARTESIAN_POINT ( 'NONE',  ( 3.974175853610068643, -2.726149789692980274, -2.409821656223221975 ) ) ;
#6133=CARTESIAN_POINT ( 'NONE',  ( 4.175326769692856210, -2.060699556488895468, 3.569236330973483806 ) ) ;
#6185=ORIENTED_EDGE ( 'NONE', *, *, #18465, .F. ) ;
#6206=EDGE_CURVE ( 'NONE', #6092, #6, #11743, .T. ) ;
#6246=DIRECTION ( 'NONE',  ( 4.440892098500626162E-16, 1.000000000000000000, 2.146163712481655900E-16 ) ) ;
#6253=CARTESIAN_POINT ( 'NONE',  ( 3.972709601346597008, -3.429395227388317924, -1.191688283765312439 ) ) ;
#6259=FACE_OUTER_BOUND ( 'NONE', #1696, .T. ) ;
#6287=DIRECTION ( 'NONE',  ( 1.000000000000000000, 4.440892098500626162E-16, -5.551115123125782702E-16 ) ) ;
#6294=CARTESIAN_POINT ( 'NONE',  ( 4.158807179406252885, 2.089320655794529635, -3.500000000000006217 ) ) ;
#6316=CARTESIAN_POINT ( 'NONE',  ( 4.104070371397483541, 4.047367226856738220, 0.000000000000000000 ) ) ;
#6357=AXIS2_PLACEMENT_3D ( 'NONE', #14893, #560, #7839 ) ;
#6388=VERTEX_POINT ( 'NONE', #9936 ) ;
#6423=DIRECTION ( 'NONE',  ( 6.621482934330019970E-16, 0.8660254037844381525, -0.5000000000000008882 ) ) ;
#6437=CARTESIAN_POINT ( 'NONE',  ( 3.972066048304799146, 3.435565134476613824, 1.180968096049749061 ) ) ;
#6450=CARTESIAN_POINT ( 'NONE',  ( 30.15500000000000114, 2.775557561562891351E-14, -2.081668171172168513E-14 ) ) ;
#6473=DIRECTION ( 'NONE',  ( -4.440892098500626162E-16, -1.000000000000000000, -2.146163712481655900E-16 ) ) ;
#6514=CARTESIAN_POINT ( 'NONE',  ( 3.973110223768740568, -0.6864646529411670972, -3.565797985667483072 ) ) ;
#6524=ORIENTED_EDGE ( 'NONE', *, *, #2322, .F. ) ;
#6588=ORIENTED_EDGE ( 'NONE', *, *, #22056, .T. ) ;
#6627=CARTESIAN_POINT ( 'NONE',  ( 0.02993401039713689329, -2.688325911136451474, 2.343682934607763890 ) ) ;
#6630=CARTESIAN_POINT ( 'NONE',  ( 3.958484000408295955, -2.327740518749134679, 2.968235154689755628 ) ) ;
#6641=VECTOR ( 'NONE', #7338, 1000.000000000000000 ) ;
#6645=B_SPLINE_CURVE_WITH_KNOTS ( 'NONE', 3,
 ( #10239, #8368, #14250, #17413, #1200, #6838, #17529, #19537, #3202, #14010, #4834, #19187, #8487, #3428, #15646, #3075 ),
 .UNSPECIFIED., .F., .F.,
 ( 4, 3, 3, 3, 3, 4 ),
 ( -2.111273352579606344E-06, 0.000000000000000000, 3.519286887794061597E-05, 7.191842652068370593E-05, 0.0001049868727093651019, 0.0001382836236822192633 ),
 .UNSPECIFIED. ) ;
#6665=CARTESIAN_POINT ( 'NONE',  ( 4.030867648404665715, 3.732851566701369528, 0.5345114293586462617 ) ) ;
#6711=ORIENTED_EDGE ( 'NONE', *, *, #10523, .T. ) ;
#6742=CARTESIAN_POINT ( 'NONE',  ( 3.961557105775642462, -1.423285172353593087, 3.499999999999995559 ) ) ;
#6755=ORIENTED_EDGE ( 'NONE', *, *, #22468, .F. ) ;
#6761=CARTESIAN_POINT ( 'NONE',  ( 4.071447262713884463, -2.020725942163688504, 3.499999999999997780 ) ) ;
#6762=ORIENTED_EDGE ( 'NONE', *, *, #5386, .T. ) ;
#6768=DIRECTION ( 'NONE',  ( 5.551115123125782702E-16, 1.201780285297635172E-31, -1.000000000000000000 ) ) ;
#6838=CARTESIAN_POINT ( 'NONE',  ( 4.165266963751727225, -4.099263933823985795, 2.410680203327883803E-15 ) ) ;
#6842=ORIENTED_EDGE ( 'NONE', *, *, #20032, .F. ) ;
#6865=CARTESIAN_POINT ( 'NONE',  ( 4.630153689607046985, -1.834136773469866309E-30, -5.371010071662817076 ) ) ;
#6939=AXIS2_PLACEMENT_3D ( 'NONE', #20308, #7264, #16637 ) ;
#6945=ORIENTED_EDGE ( 'NONE', *, *, #10523, .F. ) ;
#6958=CARTESIAN_POINT ( 'NONE',  ( 0.2182387239031264026, 1.693823289467349946, -3.500000000000008438 ) ) ;
#6966=FACE_OUTER_BOUND ( 'NONE', #20592, .T. ) ;
#6970=EDGE_CURVE ( 'NONE', #20034, #14654, #11155, .T. ) ;
#7007=VERTEX_POINT ( 'NONE', #5432 ) ;
#7038=CARTESIAN_POINT ( 'NONE',  ( 4.033901012036245959, 3.740908793663585197, -0.5205559028931702192 ) ) ;
#7039=CARTESIAN_POINT ( 'NONE',  ( 4.050536630291686535, 3.778525289263165998, 0.5912575323401342287 ) ) ;
#7063=VECTOR ( 'NONE', #22344, 1000.000000000000000 ) ;
#7067=( NAMED_UNIT ( * ) PLANE_ANGLE_UNIT ( ) SI_UNIT ( $, .RADIAN. ) );
#7085=CARTESIAN_POINT ( 'NONE',  ( 0.000000000000000000, 0.000000000000000000, 3.499999999999999556 ) ) ;
#7086=CARTESIAN_POINT ( 'NONE',  ( 3.973110223767139626, 2.264800795684280898E-11, 3.565797985667429781 ) ) ;
#7117=ADVANCED_FACE ( 'NONE', ( #6966 ), #1893, .F. ) ;
#7118=CARTESIAN_POINT ( 'NONE',  ( 4.055492966679436151, -3.795017426214147171, 0.5629142681438522589 ) ) ;
#7119=MECHANICAL_DESIGN_GEOMETRIC_PRESENTATION_REPRESENTATION('',(#18367),#1835);
#7121=ADVANCED_FACE ( 'NONE', ( #9639 ), #7447, .T. ) ;
#7152=EDGE_CURVE ( 'NONE', #22156, #8438, #1047, .T. ) ;
#7157=CARTESIAN_POINT ( 'NONE',  ( 4.086376042167601419, 1.979461949354208938, -3.571471332069177773 ) ) ;
#7190=CARTESIAN_POINT ( 'NONE',  ( 5.599999999999994316, 2.020725942163688504, -3.500000000000005773 ) ) ;
#7238=VECTOR ( 'NONE', #9720, 1000.000000000000000 ) ;
#7257=VECTOR ( 'NONE', #8423, 1000.000000000000000 ) ;
#7264=DIRECTION ( 'NONE',  ( 1.000000000000000000, 4.440892098500626162E-16, 5.551115123125782702E-16 ) ) ;
#7292=CIRCLE ( 'NONE', #2391, 5.200000000000001066 ) ;
#7338=DIRECTION ( 'NONE',  ( 0.3420201433256626622, 1.518874552022986003E-16, -0.9396926207859105373 ) ) ;
#7393=VERTEX_POINT ( 'NONE', #19624 ) ;
#7447=CONICAL_SURFACE ( 'NONE', #10449, 3.499999999999999556, 1.047197551196600074 ) ;
#7450=CARTESIAN_POINT ( 'NONE',  ( 0.1217565302851134484, 3.710888496608927056, -0.5725525826504704874 ) ) ;
#7459=AXIS2_PLACEMENT_3D ( 'NONE', #9865, #1167, #3040 ) ;
#7490=CARTESIAN_POINT ( 'NONE',  ( 4.175813232069142344, 4.122719923832743660, 0.000000000000000000 ) ) ;
#7523=B_SPLINE_CURVE_WITH_KNOTS ( 'NONE', 3,
 ( #17248, #18798, #15139, #9745, #17010 ),
 .UNSPECIFIED., .F., .F.,
 ( 4, 1, 4 ),
 ( 0.000000000000000000, 0.002020725942163689639, 0.004041451884327379278 ),
 .UNSPECIFIED. ) ;
#7528=CARTESIAN_POINT ( 'NONE',  ( 0.000000000000000000, -3.031088913245536087, -1.749999999999996447 ) ) ;
#7534=CARTESIAN_POINT ( 'NONE',  ( 4.180231891692617552, -2.049421325483212986, -3.591231015387279069 ) ) ;
#7562=ORIENTED_EDGE ( 'NONE', *, *, #6970, .T. ) ;
#7572=CARTESIAN_POINT ( 'NONE',  ( 0.1217565302851104925, 2.351289329882151335, 2.927447417349534842 ) ) ;
#7581=FACE_OUTER_BOUND ( 'NONE', #13950, .T. ) ;
#7607=( BOUNDED_SURFACE ( )  B_SPLINE_SURFACE ( 3, 2, ( 
 ( #13702, #6294, #4389 ),
 ( #20879, #11571, #7821 ),
 ( #17089, #4628, #10048 ),
 ( #4747, #10162, #20649 ),
 ( #11916, #2750, #8168 ),
 ( #4517, #14987, #15335 ) ),
 .UNSPECIFIED., .F., .F., .F. ) 
 B_SPLINE_SURFACE_WITH_KNOTS ( ( 4, 2, 4 ),
 ( 3, 3 ),
 ( 0.01652267773200354062, 0.01858309280828998253, 0.02064350788457642444 ),
 ( 0.000000000000000000, 1.000000000000000000 ),
 .UNSPECIFIED. ) 
 GEOMETRIC_REPRESENTATION_ITEM ( )  RATIONAL_B_SPLINE_SURFACE ( (
 ( 1.000000000000000000, 0.8047780975688280103, 1.000000000000000000),
 ( 1.000000000000000000, 0.8123789546318919141, 1.000000000000000000),
 ( 1.000000000000000000, 0.8190677982996300566, 1.000000000000000000),
 ( 1.000000000000000000, 0.8192346069544601539, 1.000000000000000000),
 ( 1.000000000000000000, 0.8126126759774594532, 1.000000000000000000),
 ( 1.000000000000000000, 0.8047712639312011307, 1.000000000000000000) ) ) 
 REPRESENTATION_ITEM ( '' )  SURFACE ( )  );
#7621=ADVANCED_FACE ( 'NONE', ( #2666 ), #12411, .F. ) ;
#7646=CONICAL_SURFACE ( 'NONE', #2755, 3.499999999999999556, 1.047197551196600074 ) ;
#7706=ORIENTED_EDGE ( 'NONE', *, *, #1025, .T. ) ;
#7725=CARTESIAN_POINT ( 'NONE',  ( 4.093692494532772841, 4.043567292011542413, 4.394662665088411898E-17 ) ) ;
#7757=CARTESIAN_POINT ( 'NONE',  ( 4.180345304246198879, -4.135116856707397481, 0.02129519942689462111 ) ) ;
#7793=VECTOR ( 'NONE', #998, 1000.000000000000000 ) ;
#7821=CARTESIAN_POINT ( 'NONE',  ( 4.055487192203090174, 1.409979666030529266, -3.568038521265504137 ) ) ;
#7822=EDGE_CURVE ( 'NONE', #22156, #9451, #11717, .T. ) ;
#7839=DIRECTION ( 'NONE',  ( 5.551115123125782702E-16, 1.201780285297635172E-31, -1.000000000000000000 ) ) ;
#7842=CARTESIAN_POINT ( 'NONE',  ( 4.175326769692856210, 4.121399112977853996, -1.392133645916858894E-19 ) ) ;
#7852=CARTESIAN_POINT ( 'NONE',  ( -1.170176016631815524E-15, 0.3423821193871265378, 3.499999999999994227 ) ) ;
#7870=DIRECTION ( 'NONE',  ( 1.000000000000000000, 4.440892098500626162E-16, 0.000000000000000000 ) ) ;
#7876=CARTESIAN_POINT ( 'NONE',  ( 4.142654963991857286, 2.035398498734349193, -3.525413613457316409 ) ) ;
#7886=CYLINDRICAL_SURFACE ( 'NONE', #12156, 2.500000000000001332 ) ;
#7892=CARTESIAN_POINT ( 'NONE',  ( 4.175075985190096262, -2.060370777630097905, 3.568666869285575860 ) ) ;
#7927=DIRECTION ( 'NONE',  ( -1.070367811204228886E-16, -0.8660254037844381525, -0.5000000000000009992 ) ) ;
#7953=DIRECTION ( 'NONE',  ( 0.000000000000000000, 0.000000000000000000, 1.000000000000000000 ) ) ;
#7964=CARTESIAN_POINT ( 'NONE',  ( 30.60000000000000142, 2.775557561562891351E-14, -2.081668171172168513E-14 ) ) ;
#7976=CIRCLE ( 'NONE', #8342, 2.500000000000001332 ) ;
#7994=CARTESIAN_POINT ( 'NONE',  ( 4.104070371397483541, 2.023683613428369110, -3.505122836902508698 ) ) ;
#8026=ORIENTED_EDGE ( 'NONE', *, *, #3740, .T. ) ;
#8036=CARTESIAN_POINT ( 'NONE',  ( 5.599999999999992539, 8.245366548881324970E-15, -2.500000000000001332 ) ) ;
#8038=EDGE_LOOP ( 'NONE', ( #21817, #11917 ) ) ;
#8055=EDGE_LOOP ( 'NONE', ( #5696, #22004, #20597, #17603 ) ) ;
#8071=CARTESIAN_POINT ( 'NONE',  ( 4.071447262713884463, 4.041451884327383226, 0.000000000000000000 ) ) ;
#8102=FACE_OUTER_BOUND ( 'NONE', #18673, .T. ) ;
#8119=B_SPLINE_CURVE_WITH_KNOTS ( 'NONE', 3,
 ( #17201, #10266, #8504, #22745, #13912 ),
 .UNSPECIFIED., .F., .F.,
 ( 4, 1, 4 ),
 ( 0.000000000000000000, 0.002020725942163689639, 0.004041451884327379278 ),
 .UNSPECIFIED. ) ;
#8132=CARTESIAN_POINT ( 'NONE',  ( 30.15500000000000114, 2.775557561562891351E-14, 2.499999999999981348 ) ) ;
#8153=CARTESIAN_POINT ( 'NONE',  ( 4.158921614371303477, 1.986121848748768404, -3.559936047944503912 ) ) ;
#8161=CARTESIAN_POINT ( 'NONE',  ( 4.052432342741364657, 1.393590342654231984, 3.567979436357292755 ) ) ;
#8164=CARTESIAN_POINT ( 'NONE',  ( 0.1388410611046090315, -2.351840044243034278, 2.926493552096019357 ) ) ;
#8168=CARTESIAN_POINT ( 'NONE',  ( 4.052416734886713279, -1.393505408945056478, -3.567979131523966174 ) ) ;
#8169=PRODUCT ( 'hex flange bolt small_iso_ISO 4162 - M5 x 25 x 16-N', 'hex flange bolt small_iso_ISO 4162 - M5 x 25 x 16-N', '', ( #11285 ) ) ;
#8224=EDGE_CURVE ( 'NONE', #6092, #17297, #7523, .T. ) ;
#8247=EDGE_CURVE ( 'NONE', #14654, #12775, #15857, .T. ) ;
#8342=AXIS2_PLACEMENT_3D ( 'NONE', #10043, #10269, #20875 ) ;
#8368=CARTESIAN_POINT ( 'NONE',  ( 4.175572532730925879, -4.122058607836116551, -1.269985433432320179E-15 ) ) ;
#8398=EDGE_CURVE ( 'NONE', #6092, #2560, #4687, .T. ) ;
#8399=CARTESIAN_POINT ( 'NONE',  ( 4.050880675075942072, -1.379097446046187558, -3.567934390854431204 ) ) ;
#8408=CARTESIAN_POINT ( 'NONE',  ( 3.948103430091018495, -2.682758828852505051, 2.353325403973639318 ) ) ;
#8423=DIRECTION ( 'NONE',  ( -1.000000000000000000, -4.440892098500626162E-16, 5.551115123125782702E-16 ) ) ;
#8438=VERTEX_POINT ( 'NONE', #21270 ) ;
#8448=CARTESIAN_POINT ( 'NONE',  ( 4.175813232069142344, 2.061359961916371830, 3.570380186727395433 ) ) ;
#8487=CARTESIAN_POINT ( 'NONE',  ( 4.104070371397483541, -4.047367226856738220, 0.000000000000000000 ) ) ;
#8491=ORIENTED_EDGE ( 'NONE', *, *, #8498, .F. ) ;
#8498=EDGE_CURVE ( 'NONE', #6, #12162, #14479, .T. ) ;
#8504=CARTESIAN_POINT ( 'NONE',  ( 3.806834918298641401, 2.168404344971008868E-16, 3.499999999999994227 ) ) ;
#8508=CARTESIAN_POINT ( 'NONE',  ( 4.180231680468788902, -2.085385483809538254, 3.570466434508600351 ) ) ;
#8553=ADVANCED_FACE ( 'NONE', ( #4032 ), #14768, .T. ) ;
#8646=CARTESIAN_POINT ( 'NONE',  ( 4.175813232069142344, 2.061359961916364725, -3.570380186727397209 ) ) ;
#8649=CARTESIAN_POINT ( 'NONE',  ( 0.000000000000000000, 0.000000000000000000, 0.000000000000000000 ) ) ;
#8650=DIRECTION ( 'NONE',  ( 4.844685039213900252E-16, 1.201780285297635172E-31, -1.000000000000000000 ) ) ;
#8663=ORIENTED_EDGE ( 'NONE', *, *, #4306, .F. ) ;
#8764=CARTESIAN_POINT ( 'NONE',  ( 0.000000000000000000, 0.000000000000000000, 0.000000000000000000 ) ) ;
#8782=FILL_AREA_STYLE ('',( #5129 ) ) ;
#8797=CARTESIAN_POINT ( 'NONE',  ( 4.082498951862915781, -2.020725942163695166, -3.500000000000000444 ) ) ;
#8827=CARTESIAN_POINT ( 'NONE',  ( 0.3126073911696447549, -4.041451884327383226, 0.000000000000000000 ) ) ;
#8862=ADVANCED_FACE ( 'NONE', ( #9194 ), #15875, .T. ) ;
#8880=ORIENTED_EDGE ( 'NONE', *, *, #6206, .F. ) ;
#8956=ADVANCED_FACE ( 'NONE', ( #16802 ), #7886, .T. ) ;
#8959=B_SPLINE_CURVE_WITH_KNOTS ( 'NONE', 3,
 ( #1221, #8399, #6514, #10039 ),
 .UNSPECIFIED., .F., .F.,
 ( 4, 4 ),
 ( 0.000000000000000000, 0.002080789711329279756 ),
 .UNSPECIFIED. ) ;
#8966=EDGE_LOOP ( 'NONE', ( #3411, #6711, #17573, #17677, #20739, #11819, #6762 ) ) ;
#9004=DIRECTION ( 'NONE',  ( -5.551115123125782702E-16, -1.201780285297635172E-31, 1.000000000000000000 ) ) ;
#9027=CARTESIAN_POINT ( 'NONE',  ( 3.972709601346593455, 3.429395227388313927, 1.191688283765304890 ) ) ;
#9041=AXIS2_PLACEMENT_3D ( 'NONE', #22395, #2507, #758 ) ;
#9050=CARTESIAN_POINT ( 'NONE',  ( 4.071447262713884463, -4.041451884327383226, 0.000000000000000000 ) ) ;
#9061=CARTESIAN_POINT ( 'NONE',  ( 0.1381419387168565938, -1.355287006802375460, 3.499999999999994227 ) ) ;
#9091=CARTESIAN_POINT ( 'NONE',  ( 0.000000000000000000, 0.000000000000000000, 0.000000000000000000 ) ) ;
#9102=CARTESIAN_POINT ( 'NONE',  ( 4.175326769692856210, 2.060699556488912343, 3.569236330973476701 ) ) ;
#9173=CARTESIAN_POINT ( 'NONE',  ( 4.050480423730732582, -1.376911654797400075, 3.567926555162021174 ) ) ;
#9179=CONICAL_SURFACE ( 'NONE', #9545, 3.499999999999999556, 1.047197551196600074 ) ;
#9194=FACE_OUTER_BOUND ( 'NONE', #1031, .T. ) ;
#9199=CARTESIAN_POINT ( 'NONE',  ( 4.175572532730925879, -2.061029303918044064, 3.569807470274392269 ) ) ;
#9256=CARTESIAN_POINT ( 'NONE',  ( 4.114405500665259119, -2.025575754679715068, -3.508400121684936313 ) ) ;
#9285=CARTESIAN_POINT ( 'NONE',  ( 5.599999999999995204, 7.939204849094524965E-15, 2.500000000000001332 ) ) ;
#9296=CARTESIAN_POINT ( 'NONE',  ( 3.880206590543185730, -2.665671387532593251, -2.382921720510934094 ) ) ;
#9297=VECTOR ( 'NONE', #14904, 1000.000000000000114 ) ;
#9360=EDGE_CURVE ( 'NONE', #2500, #20007, #7292, .T. ) ;
#9389=LINE ( 'NONE', #11481, #9297 ) ;
#9418=CARTESIAN_POINT ( 'NONE',  ( 3.948103430090708521, -3.379418997638742539, -1.146674596026139303 ) ) ;
#9448=ORIENTED_EDGE ( 'NONE', *, *, #20032, .T. ) ;
#9451=VERTEX_POINT ( 'NONE', #10198 ) ;
#9479=B_SPLINE_CURVE_WITH_KNOTS ( 'NONE', 3,
 ( #1452, #2137, #2259, #14725, #20031, #19921 ),
 .UNSPECIFIED., .F., .F.,
 ( 4, 2, 4 ),
 ( 0.002044882221487538416, 0.003063384235218498917, 0.004081886248949459853 ),
 .UNSPECIFIED. ) ;
#9490=AXIS2_PLACEMENT_3D ( 'NONE', #8764, #5246, #9004 ) ;
#9522=CARTESIAN_POINT ( 'NONE',  ( 0.2174200650117597278, -3.876582599186216171, -0.2855619784720702103 ) ) ;
#9545=AXIS2_PLACEMENT_3D ( 'NONE', #5838, #6287, #18632 ) ;
#9550=CARTESIAN_POINT ( 'NONE',  ( 4.151274195509686571, -2.039912954708743786, 3.533232880573495827 ) ) ;
#9594=EDGE_LOOP ( 'NONE', ( #21082, #11337, #15966, #6755, #19932 ) ) ;
#9600=FACE_OUTER_BOUND ( 'NONE', #10688, .T. ) ;
#9639=FACE_OUTER_BOUND ( 'NONE', #20302, .T. ) ;
#9641=VERTEX_POINT ( 'NONE', #17488 ) ;
#9655=CARTESIAN_POINT ( 'NONE',  ( 4.170895651974850793, -2.054890354522706186, 3.559174498016318466 ) ) ;
#9703=CARTESIAN_POINT ( 'NONE',  ( 5.599999999999994316, 4.041451884327383226, -1.734723475976807094E-15 ) ) ;
#9720=DIRECTION ( 'NONE',  ( -0.7071067811865462405, -3.140184917367542938E-16, 0.7071067811865489050 ) ) ;
#9744=ORIENTED_EDGE ( 'NONE', *, *, #12634, .F. ) ;
#9745=CARTESIAN_POINT ( 'NONE',  ( 3.951447005078448260, 3.704664227300101587, 0.5833333333333330373 ) ) ;
#9751=DIRECTION ( 'NONE',  ( -1.000000000000000000, -4.440892098500626162E-16, 5.551115123125782702E-16 ) ) ;
#9762=CARTESIAN_POINT ( 'NONE',  ( 4.158413352280815545, 2.044871626972824430, -3.541821552872970180 ) ) ;
#9769=CARTESIAN_POINT ( 'NONE',  ( 5.599999999999994316, 2.020725942163688504, 3.499999999999997780 ) ) ;
#9824=EDGE_CURVE ( 'NONE', #4649, #18414, #22654, .T. ) ;
#9845=CARTESIAN_POINT ( 'NONE',  ( 4.055492966679643096, 2.385006769473020150, 3.005124364834455442 ) ) ;
#9865=CARTESIAN_POINT ( 'NONE',  ( 4.630153689607049650, 0.000000000000000000, 0.000000000000000000 ) ) ;
#9931=CARTESIAN_POINT ( 'NONE',  ( 3.958491816110303319, 1.406739583089060774, 3.499999999999996003 ) ) ;
#9932=FACE_OUTER_BOUND ( 'NONE', #12262, .T. ) ;
#9936=CARTESIAN_POINT ( 'NONE',  ( 0.000000000000000000, 0.000000000000000000, -3.499999999999996003 ) ) ;
#9954=DIRECTION ( 'NONE',  ( -2.586960666708589311E-16, 0.5000000000000008882, 0.8660254037844381525 ) ) ;
#9966=CARTESIAN_POINT ( 'NONE',  ( -1.757169849079045659E-15, 3.202582148906729653, 1.452965002680431050 ) ) ;
#9970=CARTESIAN_POINT ( 'NONE',  ( 3.878096787214414753, 3.381939201670116635, 1.142309474598441232 ) ) ;
#9974=ADVANCED_FACE ( 'NONE', ( #11929 ), #2420, .F. ) ;
#10023=EDGE_CURVE ( 'NONE', #20684, #774, #1580, .T. ) ;
#10039=CARTESIAN_POINT ( 'NONE',  ( 3.973110223767139626, -2.262956479381524922E-11, -3.565797985667441328 ) ) ;
#10043=CARTESIAN_POINT ( 'NONE',  ( 5.599999999999994316, 0.000000000000000000, 0.000000000000000000 ) ) ;
#10047=PLANE ( 'NONE',  #22093 ) ;
#10048=CARTESIAN_POINT ( 'NONE',  ( 3.974167765203683089, 0.7238254970432166369, -3.565825589389269190 ) ) ;
#10053=VERTEX_POINT ( 'NONE', #6761 ) ;
#10063=ORIENTED_EDGE ( 'NONE', *, *, #12634, .T. ) ;
#10162=CARTESIAN_POINT ( 'NONE',  ( 3.948111298834961591, -0.6968132764971709525, -3.499999999999851230 ) ) ;
#10195=CARTESIAN_POINT ( 'NONE',  ( 4.170895651974849017, 2.054890354522667106, 3.559174498016339339 ) ) ;
#10198=CARTESIAN_POINT ( 'NONE',  ( 4.175813232069142344, 4.122719923832743660, 0.000000000000000000 ) ) ;
#10209=DIRECTION ( 'NONE',  ( -1.000000000000000000, -4.440892098500626162E-16, 5.551115123125782702E-16 ) ) ;
#10215=VERTEX_POINT ( 'NONE', #16609 ) ;
#10239=CARTESIAN_POINT ( 'NONE',  ( 4.175813232069142344, -4.122719923832743660, 0.000000000000000000 ) ) ;
#10240=AXIS2_PLACEMENT_3D ( 'NONE', #784, #6423, #9954 ) ;
#10266=CARTESIAN_POINT ( 'NONE',  ( 3.951447005078448260, -1.347150628109125226, 3.499999999999996891 ) ) ;
#10269=DIRECTION ( 'NONE',  ( -1.000000000000000000, -4.440892098500626162E-16, 5.551115123125782702E-16 ) ) ;
#10273=CARTESIAN_POINT ( 'NONE',  ( 4.180345304246195326, -2.049116244671344678, 3.591763845239302366 ) ) ;
#10276=AXIS2_PLACEMENT_3D ( 'NONE', #14922, #5653, #7870 ) ;
#10317=CARTESIAN_POINT ( 'NONE',  ( 4.142654963991854622, 2.035398498734347417, 3.525413613457306639 ) ) ;
#10320=CARTESIAN_POINT ( 'NONE',  ( 4.180231891692618440, 4.134807952925578789, 0.02076457676760740112 ) ) ;
#10345=ORIENTED_EDGE ( 'NONE', *, *, #23239, .T. ) ;
#10351=CARTESIAN_POINT ( 'NONE',  ( 30.60000000000000142, 2.800724053285369664E-14, -2.055000000000020144 ) ) ;
#10449=AXIS2_PLACEMENT_3D ( 'NONE', #4106, #20117, #14930 ) ;
#10459=AXIS2_PLACEMENT_3D ( 'NONE', #17615, #5502, #18086 ) ;
#10462=VERTEX_POINT ( 'NONE', #8827 ) ;
#10465=VECTOR ( 'NONE', #15695, 1000.000000000000000 ) ;
#10519=CIRCLE ( 'NONE', #13122, 3.499999999999999556 ) ;
#10523=EDGE_CURVE ( 'NONE', #3580, #17187, #13016, .T. ) ;
#10539=( NAMED_UNIT ( * ) SI_UNIT ( $, .STERADIAN. ) SOLID_ANGLE_UNIT ( ) );
#10604=CONICAL_SURFACE ( 'NONE', #13245, 5.371010071662833063, 1.221730476396037490 ) ;
#10619=CARTESIAN_POINT ( 'NONE',  ( 4.180231891692618440, -4.134807952925569907, -0.02076457676760569415 ) ) ;
#10626=VERTEX_POINT ( 'NONE', #9285 ) ;
#10632=EDGE_LOOP ( 'NONE', ( #17631, #9448, #2695, #18729 ) ) ;
#10636=CARTESIAN_POINT ( 'NONE',  ( 5.599999999999994316, -2.020725942163695166, -3.500000000000007550 ) ) ;
#10645=CARTESIAN_POINT ( 'NONE',  ( 0.000000000000000000, 0.000000000000000000, 0.000000000000000000 ) ) ;
#10656=SURFACE_STYLE_USAGE ( .BOTH. , #17597 ) ;
#10686=CARTESIAN_POINT ( 'NONE',  ( 5.100000000000007638, 0.000000000000000000, 0.000000000000000000 ) ) ;
#10688=EDGE_LOOP ( 'NONE', ( #12893, #427, #16876, #14698, #22357, #2176 ) ) ;
#10739=CARTESIAN_POINT ( 'NONE',  ( 3.974175853610027342, -3.450041667725643801, 1.156004144283955704 ) ) ;
#10760=CARTESIAN_POINT ( 'NONE',  ( 5.599999999999994316, -2.020725942163695166, -3.500000000000007550 ) ) ;
#10765=( BOUNDED_SURFACE ( )  B_SPLINE_SURFACE ( 3, 2, ( 
 ( #13801, #1343, #8508 ),
 ( #6742, #995, #13914 ),
 ( #4966, #15783, #2744 ),
 ( #21229, #5095, #18862 ),
 ( #9931, #20874, #8161 ),
 ( #15329, #13574, #20759 ) ),
 .UNSPECIFIED., .F., .F., .F. ) 
 B_SPLINE_SURFACE_WITH_KNOTS ( ( 4, 2, 4 ),
 ( 3, 3 ),
 ( 0.01651732063679901830, 0.01857756227444014308, 0.02063780391208126438 ),
 ( 0.000000000000000000, 1.000000000000000000 ),
 .UNSPECIFIED. ) 
 GEOMETRIC_REPRESENTATION_ITEM ( )  RATIONAL_B_SPLINE_SURFACE ( (
 ( 1.000000000000000000, 0.8047781231227495446, 1.000000000000000000),
 ( 1.000000000000000000, 0.8123782108665584811, 1.000000000000000000),
 ( 1.000000000000000000, 0.8190665102132670405, 1.000000000000000000),
 ( 1.000000000000000000, 0.8192358432844795146, 1.000000000000000000),
 ( 1.000000000000000000, 0.8126132624434716512, 1.000000000000000000),
 ( 1.000000000000000000, 0.8047712436238877443, 1.000000000000000000) ) ) 
 REPRESENTATION_ITEM ( '' )  SURFACE ( )  );
#10782=CARTESIAN_POINT ( 'NONE',  ( 4.175572532730925879, -2.061029303918069377, -3.569807470274383832 ) ) ;
#10787=TOROIDAL_SURFACE ( 'NONE', #20931, 5.200000000000001066, 0.4999999999999978351 ) ;
#10817=LINE ( 'NONE', #10351, #14826 ) ;
#10823=CARTESIAN_POINT ( 'NONE',  ( 0.2175679805410084544, -1.691499766303321106, 3.499999999999993783 ) ) ;
#10824=CIRCLE ( 'NONE', #322, 2.500000000000001332 ) ;
#10851=B_SPLINE_CURVE_WITH_KNOTS ( 'NONE', 3,
 ( #2373, #16712, #22254, #7086 ),
 .UNSPECIFIED., .F., .F.,
 ( 4, 4 ),
 ( 0.000000000000000000, 0.002080789711329261542 ),
 .UNSPECIFIED. ) ;
#10890=CARTESIAN_POINT ( 'NONE',  ( 4.158413352280815545, -2.044871626972824430, -3.541821552872962187 ) ) ;
#10914=CARTESIAN_POINT ( 'NONE',  ( 3.973110223765528914, -0.6902454861566355016, 3.565797985667388037 ) ) ;
#10916=CARTESIAN_POINT ( 'NONE',  ( 0.000000000000000000, 0.000000000000000000, 3.499999999999999556 ) ) ;
#10951=DIRECTION ( 'NONE',  ( 1.000000000000000000, 4.440892098500626162E-16, -5.551115123125782702E-16 ) ) ;
#10967=ORIENTED_EDGE ( 'NONE', *, *, #22043, .F. ) ;
#11007=CARTESIAN_POINT ( 'NONE',  ( 4.104070371397483541, -2.023683613428369110, -3.505122836902508698 ) ) ;
#11008=AXIS2_PLACEMENT_3D ( 'NONE', #3511, #3284, #12436 ) ;
#11080=CARTESIAN_POINT ( 'NONE',  ( 4.630153689607052314, 6.454774016259431095E-31, -5.371010071662833063 ) ) ;
#11100=CARTESIAN_POINT ( 'NONE',  ( 0.000000000000000000, 0.000000000000000000, 0.000000000000000000 ) ) ;
#11155=B_SPLINE_CURVE_WITH_KNOTS ( 'NONE', 3,
 ( #25, #10823, #9061, #19655, #15992, #7085 ),
 .UNSPECIFIED., .F., .F.,
 ( 4, 2, 4 ),
 ( 0.003805860999069545295, 0.004828937044845087005, 0.005852013090620628716 ),
 .UNSPECIFIED. ) ;
#11171=CARTESIAN_POINT ( 'NONE',  ( 4.071447262713884463, 2.020725942163688504, -3.499999999999999556 ) ) ;
#11175=APPLICATION_CONTEXT ( 'automotive_design' ) ;
#11187=CARTESIAN_POINT ( 'NONE',  ( 4.082498951862916670, -2.020725942163687616, 3.499999999999999556 ) ) ;
#11214=DIRECTION ( 'NONE',  ( 0.000000000000000000, 0.000000000000000000, 1.000000000000000000 ) ) ;
#11254=CARTESIAN_POINT ( 'NONE',  ( 1.387778780781446070E-15, 3.061616997868387579E-16, -2.500000000000001332 ) ) ;
#11282=CARTESIAN_POINT ( 'NONE',  ( 4.158806965674304301, -1.986429158307097431, -3.559403772175838476 ) ) ;
#11285=PRODUCT_CONTEXT ( 'NONE', #11175, 'mechanical' ) ;
#11286=ORIENTED_EDGE ( 'NONE', *, *, #8247, .T. ) ;
#11314=ORIENTED_EDGE ( 'NONE', *, *, #7822, .F. ) ;
#11315=ORIENTED_EDGE ( 'NONE', *, *, #22967, .T. ) ;
#11318=CARTESIAN_POINT ( 'NONE',  ( 30.60000000000000142, 2.775557561562891351E-14, -2.081668171172168513E-14 ) ) ;
#11337=ORIENTED_EDGE ( 'NONE', *, *, #19558, .T. ) ;
#11364=CARTESIAN_POINT ( 'NONE',  ( 0.000000000000000000, 0.000000000000000000, 3.499999999999999556 ) ) ;
#11391=ADVANCED_FACE ( 'NONE', ( #7581 ), #20290, .T. ) ;
#11397=CARTESIAN_POINT ( 'NONE',  ( 4.151274195509686571, 2.039912954708743786, -3.533232880573500712 ) ) ;
#11422=CARTESIAN_POINT ( 'NONE',  ( 4.175813232069142344, -4.122719923832743660, 0.000000000000000000 ) ) ;
#11436=ORIENTED_EDGE ( 'NONE', *, *, #18893, .T. ) ;
#11445=AXIS2_PLACEMENT_3D ( 'NONE', #18831, #11644, #13775 ) ;
#11474=CARTESIAN_POINT ( 'NONE',  ( 4.114405500665259119, 4.051151509359430136, -4.376560574388856425E-17 ) ) ;
#11481=CARTESIAN_POINT ( 'NONE',  ( 4.630153689607046985, 6.577590292450076941E-16, 5.371010071662833063 ) ) ;
#11515=AXIS2_PLACEMENT_3D ( 'NONE', #14006, #14124, #24 ) ;
#11547=ORIENTED_EDGE ( 'NONE', *, *, #3490, .T. ) ;
#11553=CARTESIAN_POINT ( 'NONE',  ( 0.000000000000000000, 3.031088913245536087, 1.750000000000003331 ) ) ;
#11555=AXIS2_PLACEMENT_3D ( 'NONE', #9091, #16367, #20268 ) ;
#11571=CARTESIAN_POINT ( 'NONE',  ( 4.033895293471146282, 1.419609371826101141, -3.500000000000006217 ) ) ;
#11625=CARTESIAN_POINT ( 'NONE',  ( 1.558781775088847367E-15, -2.686816014504586736, -2.346298152288353034 ) ) ;
#11634=ORIENTED_EDGE ( 'NONE', *, *, #9360, .T. ) ;
#11644=DIRECTION ( 'NONE',  ( -1.000000000000000000, -4.440892098500626162E-16, 5.551115123125782702E-16 ) ) ;
#11660=ORIENTED_EDGE ( 'NONE', *, *, #6032, .T. ) ;
#11717=B_SPLINE_CURVE_WITH_KNOTS ( 'NONE', 3,
 ( #13946, #12178, #19363, #1489, #3262, #5130 ),
 .UNSPECIFIED., .F., .F.,
 ( 4, 2, 4 ),
 ( 0.000000000000000000, 0.002086519881787260184, 0.004173039763574519501 ),
 .UNSPECIFIED. ) ;
#11727=AXIS2_PLACEMENT_3D ( 'NONE', #13113, #22282, #650 ) ;
#11743=LINE ( 'NONE', #2818, #272 ) ;
#11751=B_SPLINE_CURVE_WITH_KNOTS ( 'NONE', 3,
 ( #17378, #15266, #11625, #15503 ),
 .UNSPECIFIED., .F., .F.,
 ( 4, 4 ),
 ( 2.380739282734603470E-07, 0.002044882221487528875 ),
 .UNSPECIFIED. ) ;
#11814=ORIENTED_EDGE ( 'NONE', *, *, #19155, .T. ) ;
#11819=ORIENTED_EDGE ( 'NONE', *, *, #22043, .T. ) ;
#11831=CARTESIAN_POINT ( 'NONE',  ( 4.175813232069142344, 4.122719923832743660, 0.000000000000000000 ) ) ;
#11849=DIRECTION ( 'NONE',  ( 5.551115123125782702E-16, 1.201780285297635172E-31, -1.000000000000000000 ) ) ;
#11851=VERTEX_POINT ( 'NONE', #23177 ) ;
#11872=ORIENTED_EDGE ( 'NONE', *, *, #19155, .F. ) ;
#11880=ORIENTED_EDGE ( 'NONE', *, *, #17014, .T. ) ;
#11895=ORIENTED_EDGE ( 'NONE', *, *, #1932, .T. ) ;
#11909=FACE_OUTER_BOUND ( 'NONE', #20969, .T. ) ;
#11916=CARTESIAN_POINT ( 'NONE',  ( 3.958476099525450209, -1.406653531810534430, -3.500000000000007105 ) ) ;
#11917=ORIENTED_EDGE ( 'NONE', *, *, #2349, .T. ) ;
#11929=FACE_OUTER_BOUND ( 'NONE', #19138, .T. ) ;
#11935=DIRECTION ( 'NONE',  ( -1.000000000000000000, -4.440892098500625176E-16, 0.000000000000000000 ) ) ;
#11942=CARTESIAN_POINT ( 'NONE',  ( 0.3126073911696447549, 2.020725942163688504, -3.499999999999996003 ) ) ;
#11947=CARTESIAN_POINT ( 'NONE',  ( 4.180345304246196214, 4.135116856707401034, -0.02129519942689707401 ) ) ;
#12027=CARTESIAN_POINT ( 'NONE',  ( 4.086376042167604972, -1.979461949354206052, 3.571471332069173776 ) ) ;
#12143=DIRECTION ( 'NONE',  ( -4.844685039213900252E-16, -1.201780285297635172E-31, 1.000000000000000000 ) ) ;
#12156=AXIS2_PLACEMENT_3D ( 'NONE', #4223, #4113, #12951 ) ;
#12162=VERTEX_POINT ( 'NONE', #17650 ) ;
#12178=CARTESIAN_POINT ( 'NONE',  ( 4.050536630291685647, 2.401306687817039265, -2.976670123173765781 ) ) ;
#12195=DIRECTION ( 'NONE',  ( 5.551115123125782702E-16, 1.201780285297635172E-31, -1.000000000000000000 ) ) ;
#12251=DIRECTION ( 'NONE',  ( -1.000000000000000000, -4.440892098500626162E-16, 5.551115123125782702E-16 ) ) ;
#12262=EDGE_LOOP ( 'NONE', ( #6842, #200, #17097, #4190 ) ) ;
#12316=CARTESIAN_POINT ( 'NONE',  ( 3.973110223767139626, 2.264800795684280898E-11, 3.565797985667429781 ) ) ;
#12318=AXIS2_PLACEMENT_3D ( 'NONE', #4876, #3131, #7953 ) ;
#12340=CARTESIAN_POINT ( 'NONE',  ( 0.03027795055833982368, 0.6888063905328563052, -3.500000000000008882 ) ) ;
#12355=ORIENTED_EDGE ( 'NONE', *, *, #23239, .F. ) ;
#12364=ADVANCED_FACE ( 'NONE', ( #9600 ), #428, .F. ) ;
#12382=CARTESIAN_POINT ( 'NONE',  ( 4.086262629614028086, -4.082406995609982658, -0.07093633357110609716 ) ) ;
#12390=ORIENTED_EDGE ( 'NONE', *, *, #2753, .T. ) ;
#12395=EDGE_CURVE ( 'NONE', #17297, #8438, #22221, .T. ) ;
#12411=( BOUNDED_SURFACE ( )  B_SPLINE_SURFACE ( 3, 2, ( 
 ( #17477, #20556, #4425 ),
 ( #2901, #1033, #9845 ),
 ( #3146, #21023, #13729 ),
 ( #9970, #4888, #6437 ),
 ( #17119, #6665, #1380 ),
 ( #15239, #1150, #11947 ) ),
 .UNSPECIFIED., .F., .F., .F. ) 
 B_SPLINE_SURFACE_WITH_KNOTS ( ( 4, 2, 4 ),
 ( 3, 3 ),
 ( 0.01651999345535505592, 0.01858032176739835006, 0.02064065007944164767 ),
 ( 0.000000000000000000, 1.000000000000000000 ),
 .UNSPECIFIED. ) 
 GEOMETRIC_REPRESENTATION_ITEM ( )  RATIONAL_B_SPLINE_SURFACE ( (
 ( 1.000000000000000000, 0.8047781103519393575, 1.000000000000000000),
 ( 1.000000000000000000, 0.8123785825606938404, 1.000000000000000000),
 ( 1.000000000000000000, 0.8190671539784832866, 1.000000000000000000),
 ( 1.000000000000000000, 0.8192352254838310976, 1.000000000000000000),
 ( 1.000000000000000000, 0.8126129677209011914, 1.000000000000000000),
 ( 1.000000000000000000, 0.8047712537969730073, 1.000000000000000000) ) ) 
 REPRESENTATION_ITEM ( '' )  SURFACE ( )  );
#12428=CARTESIAN_POINT ( 'NONE',  ( 4.030867648403866355, 2.329326259789088915, -2.965488570641591881 ) ) ;
#12431=DIRECTION ( 'NONE',  ( 6.938893903907224433E-16, 1.201780285297635172E-31, -1.000000000000000000 ) ) ;
#12436=DIRECTION ( 'NONE',  ( 5.551115123125782702E-16, 1.201780285297635172E-31, -1.000000000000000000 ) ) ;
#12442=AXIS2_PLACEMENT_3D ( 'NONE', #1393, #22929, #12195 ) ;
#12463=DIRECTION ( 'NONE',  ( -1.000000000000000000, -4.440892098500626162E-16, 5.551115123125782702E-16 ) ) ;
#12496=FACE_OUTER_BOUND ( 'NONE', #2794, .T. ) ;
#12532=( LENGTH_UNIT ( ) NAMED_UNIT ( * ) SI_UNIT ( .MILLI., .METRE. ) );
#12634=EDGE_CURVE ( 'NONE', #20007, #2500, #556, .T. ) ;
#12657=CARTESIAN_POINT ( 'NONE',  ( 4.180345304246191773, 2.049116244671347786, -3.591763845239305919 ) ) ;
#12682=CIRCLE ( 'NONE', #11555, 3.499999999999999556 ) ;
#12713=ORIENTED_EDGE ( 'NONE', *, *, #23022, .T. ) ;
#12747=CARTESIAN_POINT ( 'NONE',  ( 4.175572532730925879, 2.061029303918053834, 3.569807470274390493 ) ) ;
#12775=VERTEX_POINT ( 'NONE', #22042 ) ;
#12778=CARTESIAN_POINT ( 'NONE',  ( 4.175326769692856210, -2.060699556488970074, -3.569236330973445170 ) ) ;
#12820=B_SPLINE_CURVE_WITH_KNOTS ( 'NONE', 3,
 ( #21164, #15384, #3045, #22460 ),
 .UNSPECIFIED., .F., .F.,
 ( 4, 4 ),
 ( 2.380739282164649823E-07, 0.002044882221487533212 ),
 .UNSPECIFIED. ) ;
#12893=ORIENTED_EDGE ( 'NONE', *, *, #20481, .F. ) ;
#12915=DIRECTION ( 'NONE',  ( 0.000000000000000000, 0.000000000000000000, 1.000000000000000000 ) ) ;
#12942=CARTESIAN_POINT ( 'NONE',  ( 4.175326769692856210, 2.060699556488931883, -3.569236330973464266 ) ) ;
#12951=DIRECTION ( 'NONE',  ( -5.551115123125782702E-16, -1.201780285297635172E-31, 1.000000000000000000 ) ) ;
#13016=B_SPLINE_CURVE_WITH_KNOTS ( 'NONE', 3,
 ( #19877, #10914, #9173, #13995 ),
 .UNSPECIFIED., .F., .F.,
 ( 4, 4 ),
 ( 0.002080789711329261542, 0.004173039763574516031 ),
 .UNSPECIFIED. ) ;
#13020=CARTESIAN_POINT ( 'NONE',  ( 4.175813232069142344, 2.061359961916371830, 3.570380186727395433 ) ) ;
#13057=CARTESIAN_POINT ( 'NONE',  ( 4.114405500665259119, 2.025575754679715512, -3.508400121684937201 ) ) ;
#13080=DIRECTION ( 'NONE',  ( 1.070367811204237268E-16, 0.8660254037844387076, 0.4999999999999999445 ) ) ;
#13081=CARTESIAN_POINT ( 'NONE',  ( 3.973514160553466290, -3.435084588004190476, 1.181876024140317227 ) ) ;
#13107=DIRECTION ( 'NONE',  ( 2.586960666708586846E-16, -0.5000000000000013323, -0.8660254037844379305 ) ) ;
#13113=CARTESIAN_POINT ( 'NONE',  ( 30.60000000000000142, 2.775557561562891351E-14, -2.081668171172168513E-14 ) ) ;
#13122=AXIS2_PLACEMENT_3D ( 'NONE', #10645, #18068, #192 ) ;
#13176=CARTESIAN_POINT ( 'NONE',  ( 4.030867648404226955, -3.732851566702299007, -0.5345114293585417897 ) ) ;
#13185=ADVANCED_FACE ( 'NONE', ( #15858 ), #17162, .F. ) ;
#13226=DIRECTION ( 'NONE',  ( 5.551115123125782702E-16, 1.201780285297635172E-31, -1.000000000000000000 ) ) ;
#13245=AXIS2_PLACEMENT_3D ( 'NONE', #19917, #10951, #20026 ) ;
#13312=CARTESIAN_POINT ( 'NONE',  ( 4.175813232069142344, -2.061359961916364725, 3.570380186727395433 ) ) ;
#13346=CARTESIAN_POINT ( 'NONE',  ( 5.599999999999994316, 4.041451884327383226, 0.000000000000000000 ) ) ;
#13352=MANIFOLD_SOLID_BREP ( 'FlangeHexFillet', #21214 ) ;
#13489=CARTESIAN_POINT ( 'NONE',  ( 4.124214193018072905, 4.056676826581892215, 5.871626145799555152E-18 ) ) ;
#13529=CARTESIAN_POINT ( 'NONE',  ( 3.948103430090704968, 2.682758828852379818, -2.353325403973791641 ) ) ;
#13574=CARTESIAN_POINT ( 'NONE',  ( 4.158921784487742634, 2.089935040870095850, 3.499999999999996003 ) ) ;
#13582=FACE_OUTER_BOUND ( 'NONE', #16002, .T. ) ;
#13702=CARTESIAN_POINT ( 'NONE',  ( 4.086262841041383709, 2.102637316508702447, -3.500000000000006217 ) ) ;
#13729=CARTESIAN_POINT ( 'NONE',  ( 3.974175853609982934, 2.726149789692692504, 2.409821656223242847 ) ) ;
#13775=DIRECTION ( 'NONE',  ( 5.551115123125782702E-16, 3.966469614587832056E-31, 1.000000000000000000 ) ) ;
#13801=CARTESIAN_POINT ( 'NONE',  ( 4.086262418390197659, -2.102635014057361307, 3.499999999999995559 ) ) ;
#13807=CARTESIAN_POINT ( 'NONE',  ( 4.030867648405966008, -2.329326259789339382, 2.965488570641001687 ) ) ;
#13873=EDGE_LOOP ( 'NONE', ( #22583, #9744 ) ) ;
#13879=EDGE_LOOP ( 'NONE', ( #8880, #14967, #2410, #11872, #8491 ) ) ;
#13912=CARTESIAN_POINT ( 'NONE',  ( 4.071447262713884463, 2.020725942163688504, 3.499999999999997780 ) ) ;
#13914=CARTESIAN_POINT ( 'NONE',  ( 4.055498735588828119, -1.410041617599661290, 3.568038744583681865 ) ) ;
#13945=PRESENTATION_STYLE_ASSIGNMENT (( #10656 ) ) ;
#13946=CARTESIAN_POINT ( 'NONE',  ( 4.175813232069142344, 2.061359961916364725, -3.570380186727397209 ) ) ;
#13950=EDGE_LOOP ( 'NONE', ( #14340, #1431, #1357, #14507 ) ) ;
#13959=CARTESIAN_POINT ( 'NONE',  ( 4.086262629614028086, 4.082406995609991540, 0.07093633357110795679 ) ) ;
#13971=ADVANCED_FACE ( 'NONE', ( #15203 ), #15410, .T. ) ;
#13978=AXIS2_PLACEMENT_3D ( 'NONE', #1227, #12251, #12143 ) ;
#13986=B_SPLINE_CURVE_WITH_KNOTS ( 'NONE', 3,
 ( #4418, #9966, #6083, #19021, #15234, #15124 ),
 .UNSPECIFIED., .F., .F.,
 ( 4, 2, 4 ),
 ( 0.002044882221487523237, 0.003063384235218489810, 0.004081886248949456383 ),
 .UNSPECIFIED. ) ;
#13995=CARTESIAN_POINT ( 'NONE',  ( 4.175813232069142344, -2.061359961916364725, 3.570380186727395433 ) ) ;
#14006=CARTESIAN_POINT ( 'NONE',  ( 30.60000000000000142, 2.775557561562891351E-14, -2.081668171172168513E-14 ) ) ;
#14010=CARTESIAN_POINT ( 'NONE',  ( 4.132952817037863547, -4.063368025374519910, 0.000000000000000000 ) ) ;
#14016=ORIENTED_EDGE ( 'NONE', *, *, #2239, .F. ) ;
#14120=CARTESIAN_POINT ( 'NONE',  ( 0.3126073911696447549, -2.020725942163688504, 3.499999999999997780 ) ) ;
#14124=DIRECTION ( 'NONE',  ( -1.000000000000000000, -4.440892098500626162E-16, -5.551115123125782702E-16 ) ) ;
#14164=ORIENTED_EDGE ( 'NONE', *, *, #5386, .F. ) ;
#14194=ORIENTED_EDGE ( 'NONE', *, *, #18465, .T. ) ;
#14209=CARTESIAN_POINT ( 'NONE',  ( 3.880206590543182177, 3.396506438958478480, -1.117078279489084558 ) ) ;
#14211=CARTESIAN_POINT ( 'NONE',  ( 3.973514160553462737, 2.741076955031362949, 2.383932505289867887 ) ) ;
#14241=DIRECTION ( 'NONE',  ( -0.7071067811865462405, -2.274228861132049406E-16, -0.7071067811865489050 ) ) ;
#14250=CARTESIAN_POINT ( 'NONE',  ( 4.175326769692856210, -4.121399112977853996, -4.789320010053836886E-15 ) ) ;
#14290=ORIENTED_EDGE ( 'NONE', *, *, #4306, .T. ) ;
#14307=( NAMED_UNIT ( * ) PLANE_ANGLE_UNIT ( ) SI_UNIT ( $, .RADIAN. ) );
#14317=CARTESIAN_POINT ( 'NONE',  ( 3.958484000407092029, 2.327740518748989906, -2.968235154690015865 ) ) ;
#14340=ORIENTED_EDGE ( 'NONE', *, *, #3740, .F. ) ;
#14418=CIRCLE ( 'NONE', #10276, 0.4999999999999978351 ) ;
#14466=( LENGTH_UNIT ( ) NAMED_UNIT ( * ) SI_UNIT ( .MILLI., .METRE. ) );
#14479=B_SPLINE_CURVE_WITH_KNOTS ( 'NONE', 3,
 ( #20389, #7572, #520, #11553 ),
 .UNSPECIFIED., .F., .F.,
 ( 4, 4 ),
 ( 2.380739282131849795E-07, 0.002044882221487523237 ),
 .UNSPECIFIED. ) ;
#14507=ORIENTED_EDGE ( 'NONE', *, *, #2349, .F. ) ;
#14512=CARTESIAN_POINT ( 'NONE',  ( 4.132952817037863547, 2.031684012687259955, 3.518979934899744588 ) ) ;
#14570=EDGE_CURVE ( 'NONE', #19198, #6388, #1284, .T. ) ;
#14615=CARTESIAN_POINT ( 'NONE',  ( 4.175813232069142344, -2.061359961916364725, 3.570380186727395433 ) ) ;
#14645=CARTESIAN_POINT ( 'NONE',  ( 5.599999999999994316, -2.020725942163688504, 3.499999999999996003 ) ) ;
#14646=( BOUNDED_SURFACE ( )  B_SPLINE_SURFACE ( 3, 2, ( 
 ( #12382, #19564, #10619 ),
 ( #17809, #23233, #7118 ),
 ( #3574, #19690, #10739 ),
 ( #1232, #8408, #15568 ),
 ( #6630, #13807, #4859 ),
 ( #12027, #19215, #10273 ) ),
 .UNSPECIFIED., .F., .F., .F. ) 
 B_SPLINE_SURFACE_WITH_KNOTS ( ( 4, 2, 4 ),
 ( 3, 3 ),
 ( 0.01651999345535504551, 0.01858032176739833966, 0.02064065007944163380 ),
 ( 0.000000000000000000, 1.000000000000000000 ),
 .UNSPECIFIED. ) 
 GEOMETRIC_REPRESENTATION_ITEM ( )  RATIONAL_B_SPLINE_SURFACE ( (
 ( 1.000000000000000000, 0.8047781103519392465, 1.000000000000000000),
 ( 1.000000000000000000, 0.8123785825606634203, 1.000000000000000000),
 ( 1.000000000000000000, 0.8190671539785229216, 1.000000000000000000),
 ( 1.000000000000000000, 0.8192352254837912406, 1.000000000000000000),
 ( 1.000000000000000000, 0.8126129677209334989, 1.000000000000000000),
 ( 1.000000000000000000, 0.8047712537969733404, 1.000000000000000000) ) ) 
 REPRESENTATION_ITEM ( '' )  SURFACE ( )  );
#14654=VERTEX_POINT ( 'NONE', #10916 ) ;
#14659=CARTESIAN_POINT ( 'NONE',  ( 4.151274195509686571, -2.039912954708744675, -3.533232880573493606 ) ) ;
#14690=CARTESIAN_POINT ( 'NONE',  ( 0.02993401039714140358, -3.373851915354621145, -1.156317065392238774 ) ) ;
#14698=ORIENTED_EDGE ( 'NONE', *, *, #8247, .F. ) ;
#14725=CARTESIAN_POINT ( 'NONE',  ( 0.1388410611046089760, 2.351840044243042716, -2.926493552096025130 ) ) ;
#14768=CONICAL_SURFACE ( 'NONE', #16267, 2.054999999999999716, 0.7853981633974502774 ) ;
#14793=CARTESIAN_POINT ( 'NONE',  ( 0.03027795056225613193, 0.6888063905605182891, 3.499999999999994671 ) ) ;
#14826=VECTOR ( 'NONE', #14241, 1000.000000000000000 ) ;
#14832=ORIENTED_EDGE ( 'NONE', *, *, #4937, .T. ) ;
#14868=PLANE ( 'NONE',  #18122 ) ;
#14893=CARTESIAN_POINT ( 'NONE',  ( 0.000000000000000000, 0.000000000000000000, 0.000000000000000000 ) ) ;
#14904=DIRECTION ( 'NONE',  ( 0.3420201433256619405, 2.669666112250838244E-16, 0.9396926207859108704 ) ) ;
#14910=( BOUNDED_SURFACE ( )  B_SPLINE_SURFACE ( 3, 2, ( 
 ( #13959, #23158, #10320 ),
 ( #17489, #7038, #15725 ),
 ( #14209, #21398, #15831 ),
 ( #5268, #13529, #5388 ),
 ( #14317, #12428, #19610 ),
 ( #7157, #8153, #12657 ) ),
 .UNSPECIFIED., .F., .F., .F. ) 
 B_SPLINE_SURFACE_WITH_KNOTS ( ( 4, 2, 4 ),
 ( 3, 3 ),
 ( 0.01651999345535504551, 0.01858032176739834312, 0.02064065007944163727 ),
 ( 0.000000000000000000, 1.000000000000000000 ),
 .UNSPECIFIED. ) 
 GEOMETRIC_REPRESENTATION_ITEM ( )  RATIONAL_B_SPLINE_SURFACE ( (
 ( 1.000000000000000000, 0.8047781103519390244, 1.000000000000000000),
 ( 1.000000000000000000, 0.8123785825604538102, 1.000000000000000000),
 ( 1.000000000000000000, 0.8190671539788021427, 1.000000000000000000),
 ( 1.000000000000000000, 0.8192352254835137959, 1.000000000000000000),
 ( 1.000000000000000000, 0.8126129677211418878, 1.000000000000000000),
 ( 1.000000000000000000, 0.8047712537969714530, 1.000000000000000000) ) ) 
 REPRESENTATION_ITEM ( '' )  SURFACE ( )  );
#14922=CARTESIAN_POINT ( 'NONE',  ( 5.100000000000004974, -6.249257483547704998E-31, 5.200000000000001066 ) ) ;
#14927=B_SPLINE_CURVE_WITH_KNOTS ( 'NONE', 3,
 ( #15464, #4994, #15693, #8646 ),
 .UNSPECIFIED., .F., .F.,
 ( 4, 4 ),
 ( 0.002080789711329279756, 0.004173039763574516031 ),
 .UNSPECIFIED. ) ;
#14930=DIRECTION ( 'NONE',  ( 5.551115123125782702E-16, 1.201780285297635172E-31, -1.000000000000000000 ) ) ;
#14938=CARTESIAN_POINT ( 'NONE',  ( 0.000000000000000000, 0.000000000000000000, 0.000000000000000000 ) ) ;
#14952=DIRECTION ( 'NONE',  ( -7.027852765209222375E-16, -0.4999999999999999445, 0.8660254037844387076 ) ) ;
#14967=ORIENTED_EDGE ( 'NONE', *, *, #8224, .T. ) ;
#14975=CARTESIAN_POINT ( 'NONE',  ( 0.3126073911695753660, -2.020725942163792421, -3.499999999999996891 ) ) ;
#14987=CARTESIAN_POINT ( 'NONE',  ( 4.158921444904713383, -2.089933220600047825, -3.500000000000007105 ) ) ;
#15038=CARTESIAN_POINT ( 'NONE',  ( 4.093692494532772841, 2.021783646005771207, -3.501831996793843160 ) ) ;
#15041=B_SPLINE_CURVE_WITH_KNOTS ( 'NONE', 3,
 ( #8071, #22424, #7725, #6316, #11474, #13489, #2426, #17111, #20672, #4537, #5971, #2780, #673, #7842, #21012, #11831 ),
 .UNSPECIFIED., .F., .F.,
 ( 4, 3, 3, 3, 3, 4 ),
 ( 0.000000000000000000, 3.315506744709155554E-05, 6.608280158698816038E-05, 0.0001026520855291328406, 0.0001376952025664795836, 0.0001398064759190610195 ),
 .UNSPECIFIED. ) ;
#15053=CARTESIAN_POINT ( 'NONE',  ( 4.142654963991856398, -2.035398498734349193, 3.525413613457312412 ) ) ;
#15124=CARTESIAN_POINT ( 'NONE',  ( 0.3126073911696447549, 4.041451884327383226, 0.000000000000000000 ) ) ;
#15139=CARTESIAN_POINT ( 'NONE',  ( 3.806834918298644954, 3.031088913245544969, 1.750000000000003331 ) ) ;
#15162=CARTESIAN_POINT ( 'NONE',  ( 4.175813232069142344, 2.061359961916364725, -3.570380186727397209 ) ) ;
#15178=CARTESIAN_POINT ( 'NONE',  ( 4.175813232069142344, -4.122719923832743660, 0.000000000000000000 ) ) ;
#15202=CARTESIAN_POINT ( 'NONE',  ( 0.000000000000000000, 0.000000000000000000, -3.499999999999996003 ) ) ;
#15203=FACE_OUTER_BOUND ( 'NONE', #19807, .T. ) ;
#15234=CARTESIAN_POINT ( 'NONE',  ( 0.2174200650117545097, 3.876582599186212619, 0.2855619784720683230 ) ) ;
#15239=CARTESIAN_POINT ( 'NONE',  ( 4.086376042167605860, 4.082715877136870120, -0.07147133206917886949 ) ) ;
#15266=CARTESIAN_POINT ( 'NONE',  ( 0.1217565302851057185, -2.351289329882179757, -2.927447417349501979 ) ) ;
#15278=ADVANCED_FACE ( 'NONE', ( #20791 ), #17335, .T. ) ;
#15320=CARTESIAN_POINT ( 'NONE',  ( 0.02944718078427569982, -0.6813962075686340603, -3.500000000000010214 ) ) ;
#15329=CARTESIAN_POINT ( 'NONE',  ( 4.086376210449949475, 2.103254844323304340, 3.499999999999996447 ) ) ;
#15335=CARTESIAN_POINT ( 'NONE',  ( 4.180345136606688605, -2.085999704580135727, -3.570468642550122862 ) ) ;
#15353=CARTESIAN_POINT ( 'NONE',  ( 5.100000000000010303, 6.368163355566245256E-16, -5.200000000000001066 ) ) ;
#15384=CARTESIAN_POINT ( 'NONE',  ( 0.1217565302851110615, -3.710888496608917730, 0.5725525826504641591 ) ) ;
#15386=CARTESIAN_POINT ( 'NONE',  ( 4.071447262713884463, 2.020725942163688504, 3.499999999999997780 ) ) ;
#15410=CONICAL_SURFACE ( 'NONE', #9041, 3.499999999999999556, 1.047197551196600074 ) ;
#15448=ORIENTED_EDGE ( 'NONE', *, *, #7152, .T. ) ;
#15464=CARTESIAN_POINT ( 'NONE',  ( 3.973110223767139626, -2.262956479381524922E-11, -3.565797985667441328 ) ) ;
#15503=CARTESIAN_POINT ( 'NONE',  ( 0.000000000000000000, -3.031088913245536087, -1.749999999999996447 ) ) ;
#15550=CARTESIAN_POINT ( 'NONE',  ( 0.3126073911696447549, 2.020725942163688504, 3.499999999999997780 ) ) ;
#15568=CARTESIAN_POINT ( 'NONE',  ( 3.972066048304754737, -2.740530939476236050, 2.384802634787871689 ) ) ;
#15646=CARTESIAN_POINT ( 'NONE',  ( 4.082498951862915781, -4.041451884327383226, -6.134919877127760970E-18 ) ) ;
#15693=CARTESIAN_POINT ( 'NONE',  ( 4.050480423730732582, 1.376911654797405848, -3.567926555162023394 ) ) ;
#15695=DIRECTION ( 'NONE',  ( -1.000000000000000000, -4.440892098500626162E-16, 5.551115123125782702E-16 ) ) ;
#15725=CARTESIAN_POINT ( 'NONE',  ( 4.055492966679613787, 3.795017426214645884, -0.5629142681441038354 ) ) ;
#15783=CARTESIAN_POINT ( 'NONE',  ( 3.950250160040162051, -0.7258013381035534062, 3.499999999999996003 ) ) ;
#15831=CARTESIAN_POINT ( 'NONE',  ( 3.974175853610035780, 3.450041667725636252, -1.156004144284049850 ) ) ;
#15857=CIRCLE ( 'NONE', #2350, 3.499999999999999556 ) ;
#15858=FACE_OUTER_BOUND ( 'NONE', #19248, .T. ) ;
#15875=CONICAL_SURFACE ( 'NONE', #18907, 3.499999999999999556, 1.047197551196600074 ) ;
#15966=ORIENTED_EDGE ( 'NONE', *, *, #6206, .T. ) ;
#15977=( NAMED_UNIT ( * ) SI_UNIT ( $, .STERADIAN. ) SOLID_ANGLE_UNIT ( ) );
#15992=CARTESIAN_POINT ( 'NONE',  ( -1.030839096808483710E-15, -0.3420925509533346287, 3.499999999999994227 ) ) ;
#16002=EDGE_LOOP ( 'NONE', ( #2884, #23122, #2413, #4530, #22385 ) ) ;
#16067=CARTESIAN_POINT ( 'NONE',  ( 4.132952817037863547, -2.031684012687259955, -3.518979934899747253 ) ) ;
#16093=SURFACE_SIDE_STYLE ('',( #1981 ) ) ;
#16106=CONICAL_SURFACE ( 'NONE', #6357, 3.499999999999999556, 1.047197551196600074 ) ;
#16114=EDGE_CURVE ( 'NONE', #7007, #10053, #1477, .T. ) ;
#16144=EDGE_CURVE ( 'NONE', #18229, #20684, #16341, .T. ) ;
#16197=EDGE_CURVE ( 'NONE', #9451, #2560, #5695, .T. ) ;
#16267=AXIS2_PLACEMENT_3D ( 'NONE', #11318, #2619, #11214 ) ;
#16321=EDGE_LOOP ( 'NONE', ( #19345, #4020, #14194, #21244, #18620 ) ) ;
#16341=B_SPLINE_CURVE_WITH_KNOTS ( 'NONE', 3,
 ( #3830, #10782, #12778, #18206, #21399, #21843, #10890, #14659, #5499, #16067, #20083, #9256, #11007, #5732, #8797, #19961 ),
 .UNSPECIFIED., .F., .F.,
 ( 4, 3, 3, 3, 3, 4 ),
 ( -2.111273352580643536E-06, 0.000000000000000000, 3.519286887793932848E-05, 7.191842652068034490E-05, 0.0001049868727093635162, 0.0001382836236822177726 ),
 .UNSPECIFIED. ) ;
#16367=DIRECTION ( 'NONE',  ( 1.000000000000000000, 4.440892098500626162E-16, -5.551115123125782702E-16 ) ) ;
#16443=ORIENTED_EDGE ( 'NONE', *, *, #7822, .T. ) ;
#16448=CARTESIAN_POINT ( 'NONE',  ( 30.60000000000000142, 2.793567907494308344E-14, -2.055000000000020144 ) ) ;
#16455=CARTESIAN_POINT ( 'NONE',  ( 3.958484000406611525, -3.734437307742145329, -0.5317648453098834382 ) ) ;
#16463=EDGE_CURVE ( 'NONE', #10215, #22156, #14927, .T. ) ;
#16473=CARTESIAN_POINT ( 'NONE',  ( 4.158413352280815545, -2.044871626972824430, 3.541821552872964851 ) ) ;
#16566=EDGE_CURVE ( 'NONE', #14654, #12162, #16607, .T. ) ;
#16607=CIRCLE ( 'NONE', #9490, 3.499999999999999556 ) ;
#16609=CARTESIAN_POINT ( 'NONE',  ( 3.973110223767139626, -2.262956479381524922E-11, -3.565797985667441328 ) ) ;
#16637=DIRECTION ( 'NONE',  ( 5.551115123125782702E-16, 1.201780285297635172E-31, -1.000000000000000000 ) ) ;
#16678=CARTESIAN_POINT ( 'NONE',  ( 0.3126073911696447549, -4.041451884327383226, 0.000000000000000000 ) ) ;
#16686=ADVANCED_FACE ( 'NONE', ( #644 ), #14868, .F. ) ;
#16705=PLANE ( 'NONE',  #4171 ) ;
#16712=CARTESIAN_POINT ( 'NONE',  ( 4.050880675075942960, 1.379097446046193998, 3.567934390854428095 ) ) ;
#16758=FACE_OUTER_BOUND ( 'NONE', #3353, .T. ) ;
#16780=ORIENTED_EDGE ( 'NONE', *, *, #17014, .F. ) ;
#16802=FACE_OUTER_BOUND ( 'NONE', #5987, .T. ) ;
#16871=ORIENTED_EDGE ( 'NONE', *, *, #2239, .T. ) ;
#16876=ORIENTED_EDGE ( 'NONE', *, *, #18893, .F. ) ;
#16915=CARTESIAN_POINT ( 'NONE',  ( 3.972066048304715213, -3.435565134476332716, -1.180968096049761495 ) ) ;
#16959=DIRECTION ( 'NONE',  ( -6.621482934330023914E-16, -0.8660254037844379305, 0.5000000000000013323 ) ) ;
#16965=LINE ( 'NONE', #17086, #7793 ) ;
#17004=ORIENTED_EDGE ( 'NONE', *, *, #16463, .T. ) ;
#17010=CARTESIAN_POINT ( 'NONE',  ( 4.071447262713884463, 4.041451884327383226, 0.000000000000000000 ) ) ;
#17014=EDGE_CURVE ( 'NONE', #10053, #17187, #3152, .T. ) ;
#17069=ORIENTED_EDGE ( 'NONE', *, *, #4082, .T. ) ;
#17086=CARTESIAN_POINT ( 'NONE',  ( -1.387778780781446464E-15, -3.004450713244089682E-31, 2.500000000000001332 ) ) ;
#17089=CARTESIAN_POINT ( 'NONE',  ( 3.880198502136890770, 0.7307680362928052897, -3.500000000000006661 ) ) ;
#17097=ORIENTED_EDGE ( 'NONE', *, *, #9824, .T. ) ;
#17111=CARTESIAN_POINT ( 'NONE',  ( 4.142654963991856398, 4.070796997468703715, -6.519033156300609374E-18 ) ) ;
#17119=CARTESIAN_POINT ( 'NONE',  ( 3.958484000407115122, 3.734437307742082268, 0.5317648453099944605 ) ) ;
#17162=PLANE ( 'NONE',  #3383 ) ;
#17176=CIRCLE ( 'NONE', #20960, 2.054999999999999716 ) ;
#17187=VERTEX_POINT ( 'NONE', #22370 ) ;
#17201=CARTESIAN_POINT ( 'NONE',  ( 4.071447262713884463, -2.020725942163688504, 3.499999999999997780 ) ) ;
#17228=( GEOMETRIC_REPRESENTATION_CONTEXT ( 3 ) GLOBAL_UNCERTAINTY_ASSIGNED_CONTEXT ( ( #1328 ) ) GLOBAL_UNIT_ASSIGNED_CONTEXT ( ( #920, #14307, #5257 ) ) REPRESENTATION_CONTEXT ( 'NONE', 'WORKASPACE' ) );
#17248=CARTESIAN_POINT ( 'NONE',  ( 4.071447262713884463, 2.020725942163688504, 3.499999999999997780 ) ) ;
#17279=CARTESIAN_POINT ( 'NONE',  ( 5.599999999999994316, 2.020725942163688504, -3.500000000000005773 ) ) ;
#17297=VERTEX_POINT ( 'NONE', #19406 ) ;
#17335=CONICAL_SURFACE ( 'NONE', #1203, 5.371010071662833063, 1.221730476396037490 ) ;
#17342=B_SPLINE_CURVE_WITH_KNOTS ( 'NONE', 3,
 ( #11364, #7852, #14793, #685, #22205, #335 ),
 .UNSPECIFIED., .F., .F.,
 ( 4, 2, 4 ),
 ( 0.005852013090620628716, 0.006875955131657974020, 0.007899897172695319325 ),
 .UNSPECIFIED. ) ;
#17352=ORIENTED_EDGE ( 'NONE', *, *, #2070, .F. ) ;
#17378=CARTESIAN_POINT ( 'NONE',  ( 0.3126073911695753660, -2.020725942163792421, -3.499999999999996891 ) ) ;
#17413=CARTESIAN_POINT ( 'NONE',  ( 4.175075985190096262, -4.120741555260244660, -3.469446951953614189E-15 ) ) ;
#17425=ORIENTED_EDGE ( 'NONE', *, *, #16566, .F. ) ;
#17435=EDGE_CURVE ( 'NONE', #2500, #4523, #14418, .T. ) ;
#17441=CARTESIAN_POINT ( 'NONE',  ( 0.3126073911696447549, -2.020725942163688504, 3.499999999999997780 ) ) ;
#17448=LINE ( 'NONE', #11080, #6641 ) ;
#17450=VERTEX_POINT ( 'NONE', #16448 ) ;
#17468=DIRECTION ( 'NONE',  ( 1.000000000000000000, 4.440892098500626162E-16, -5.551115123125782702E-16 ) ) ;
#17477=CARTESIAN_POINT ( 'NONE',  ( 4.086262629614028086, 1.979770830881089294, 3.570936333571107735 ) ) ;
#17485=CARTESIAN_POINT ( 'NONE',  ( 4.082498951862915781, 2.020725942163688504, 3.499999999999997780 ) ) ;
#17488=CARTESIAN_POINT ( 'NONE',  ( 30.15500000000000114, 8.245366548881241351E-15, -2.500000000000023093 ) ) ;
#17489=CARTESIAN_POINT ( 'NONE',  ( 3.961551342853960378, 3.742715940867782365, -0.5174258321190572385 ) ) ;
#17494=APPLICATION_CONTEXT ( 'automotive_design' ) ;
#17529=CARTESIAN_POINT ( 'NONE',  ( 4.158413352280815545, -4.089743253945648860, 1.734723475976807094E-15 ) ) ;
#17550=ADVANCED_FACE ( 'NONE', ( #8102 ), #7646, .T. ) ;
#17573=ORIENTED_EDGE ( 'NONE', *, *, #4488, .T. ) ;
#17597=SURFACE_SIDE_STYLE ('',( #5008 ) ) ;
#17603=ORIENTED_EDGE ( 'NONE', *, *, #8224, .F. ) ;
#17615=CARTESIAN_POINT ( 'NONE',  ( 30.60000000000000142, 2.775557561562891351E-14, -2.081668171172168513E-14 ) ) ;
#17631=ORIENTED_EDGE ( 'NONE', *, *, #22479, .T. ) ;
#17650=CARTESIAN_POINT ( 'NONE',  ( 0.000000000000000000, 3.031088913245536087, 1.750000000000003331 ) ) ;
#17677=ORIENTED_EDGE ( 'NONE', *, *, #4713, .T. ) ;
#17727=CARTESIAN_POINT ( 'NONE',  ( 5.599999999999994316, 0.000000000000000000, 0.000000000000000000 ) ) ;
#17745=ADVANCED_FACE ( 'NONE', ( #875 ), #9179, .T. ) ;
#17809=CARTESIAN_POINT ( 'NONE',  ( 3.961551342854460867, -3.742715940867668234, 0.5174258321192414245 ) ) ;
#17856=DIRECTION ( 'NONE',  ( -1.000000000000000000, -4.440892098500626162E-16, 5.551115123125782702E-16 ) ) ;
#17871=EDGE_LOOP ( 'NONE', ( #373, #6524 ) ) ;
#17966=ORIENTED_EDGE ( 'NONE', *, *, #18691, .T. ) ;
#17996=ADVANCED_FACE ( 'NONE', ( #11909 ), #10765, .F. ) ;
#18020=STYLED_ITEM ( 'NONE', ( #3746 ), #13352 ) ;
#18068=DIRECTION ( 'NONE',  ( 1.000000000000000000, 4.440892098500626162E-16, -5.551115123125782702E-16 ) ) ;
#18086=DIRECTION ( 'NONE',  ( 0.000000000000000000, 0.000000000000000000, 1.000000000000000000 ) ) ;
#18122=AXIS2_PLACEMENT_3D ( 'NONE', #4377, #16959, #13107 ) ;
#18206=CARTESIAN_POINT ( 'NONE',  ( 4.175075985190096262, -2.060370777630153416, -3.568666869285546994 ) ) ;
#18229=VERTEX_POINT ( 'NONE', #18259 ) ;
#18244=EDGE_LOOP ( 'NONE', ( #21265, #10063, #1807, #14164 ) ) ;
#18259=CARTESIAN_POINT ( 'NONE',  ( 4.175813232069142344, -2.061359961916371830, -3.570380186727398986 ) ) ;
#18354=CARTESIAN_POINT ( 'NONE',  ( 3.961551342854305435, -2.319461885623339548, -2.982574167880875926 ) ) ;
#18365=DIRECTION ( 'NONE',  ( 5.551115123125782702E-16, 1.201780285297635172E-31, -1.000000000000000000 ) ) ;
#18367=STYLED_ITEM ( 'NONE', ( #13945 ), #19561 ) ;
#18414=VERTEX_POINT ( 'NONE', #8132 ) ;
#18464=CARTESIAN_POINT ( 'NONE',  ( 4.033901012036569256, -2.321269032827520284, -2.979444097106667577 ) ) ;
#18465=EDGE_CURVE ( 'NONE', #8438, #19198, #22, .T. ) ;
#18522=VECTOR ( 'NONE', #12463, 1000.000000000000000 ) ;
#18553=DIRECTION ( 'NONE',  ( -1.000000000000000000, -4.440892098500626162E-16, 5.551115123125782702E-16 ) ) ;
#18561=AXIS2_PLACEMENT_3D ( 'NONE', #1246, #21478, #23246 ) ;
#18586=CARTESIAN_POINT ( 'NONE',  ( 3.878096787214415642, -3.381939201670079775, -1.142309474598505181 ) ) ;
#18609=CIRCLE ( 'NONE', #12442, 3.499999999999999556 ) ;
#18620=ORIENTED_EDGE ( 'NONE', *, *, #22056, .F. ) ;
#18626=CARTESIAN_POINT ( 'NONE',  ( 0.2175679805369863662, -1.691499766289382256, -3.500000000000010214 ) ) ;
#18632=DIRECTION ( 'NONE',  ( 5.551115123125782702E-16, 1.201780285297635172E-31, -1.000000000000000000 ) ) ;
#18673=EDGE_LOOP ( 'NONE', ( #11547, #11436, #3637 ) ) ;
#18691=EDGE_CURVE ( 'NONE', #774, #11851, #11751, .T. ) ;
#18729=ORIENTED_EDGE ( 'NONE', *, *, #9824, .F. ) ;
#18773=CARTESIAN_POINT ( 'NONE',  ( 4.071447262713884463, 4.041451884327383226, 0.000000000000000000 ) ) ;
#18774=CARTESIAN_POINT ( 'NONE',  ( 30.60000000000000142, 2.775557561562891351E-14, 2.054999999999978844 ) ) ;
#18794=ORIENTED_EDGE ( 'NONE', *, *, #8498, .T. ) ;
#18798=CARTESIAN_POINT ( 'NONE',  ( 3.951447005078448260, 2.357513599190970144, 2.916666666666664742 ) ) ;
#18831=CARTESIAN_POINT ( 'NONE',  ( 5.100000000000007638, 0.000000000000000000, 0.000000000000000000 ) ) ;
#18862=CARTESIAN_POINT ( 'NONE',  ( 3.972058292797657320, 0.6948821373597494633, 3.565770528409099249 ) ) ;
#18893=EDGE_CURVE ( 'NONE', #12775, #11851, #21172, .T. ) ;
#18907=AXIS2_PLACEMENT_3D ( 'NONE', #14938, #20485, #18365 ) ;
#18966=TOROIDAL_SURFACE ( 'NONE', #11445, 5.200000000000001066, 0.4999999999999978351 ) ;
#19021=CARTESIAN_POINT ( 'NONE',  ( 0.1388410611046085874, 3.710337782248036120, 0.5735064479039790886 ) ) ;
#19075=ORIENTED_EDGE ( 'NONE', *, *, #19935, .T. ) ;
#19138=EDGE_LOOP ( 'NONE', ( #17352, #5821, #17069, #8663, #22614 ) ) ;
#19155=EDGE_CURVE ( 'NONE', #12162, #5230, #13986, .T. ) ;
#19187=CARTESIAN_POINT ( 'NONE',  ( 4.114405500665258231, -4.051151509359430136, -5.737149237780425473E-18 ) ) ;
#19192=UNCERTAINTY_MEASURE_WITH_UNIT (LENGTH_MEASURE( 1.000000000000000082E-05 ), #12532, 'distance_accuracy_value', 'NONE');
#19198=VERTEX_POINT ( 'NONE', #11942 ) ;
#19215=CARTESIAN_POINT ( 'NONE',  ( 4.158921614371306141, -1.986121848748765073, 3.559936047944500359 ) ) ;
#19248=EDGE_LOOP ( 'NONE', ( #6185, #11660, #22579, #1698, #21818 ) ) ;
#19338=ORIENTED_EDGE ( 'NONE', *, *, #3964, .T. ) ;
#19345=ORIENTED_EDGE ( 'NONE', *, *, #2903, .F. ) ;
#19363=CARTESIAN_POINT ( 'NONE',  ( 3.972709601346593011, 2.746729940827194127, -2.374099244652738694 ) ) ;
#19406=CARTESIAN_POINT ( 'NONE',  ( 4.071447262713884463, 4.041451884327383226, 0.000000000000000000 ) ) ;
#19481=EDGE_CURVE ( 'NONE', #18229, #10215, #8959, .T. ) ;
#19525=DIRECTION ( 'NONE',  ( -5.551115123125782702E-16, -2.146163712481653435E-16, 1.000000000000000000 ) ) ;
#19537=CARTESIAN_POINT ( 'NONE',  ( 4.151274195509685683, -4.079825909417488461, 1.030604039451950803E-15 ) ) ;
#19558=EDGE_CURVE ( 'NONE', #10053, #6092, #8119, .T. ) ;
#19561=ADVANCED_BREP_SHAPE_REPRESENTATION ( '', ( #13352, #22115 ), #17228 ) ;
#19564=CARTESIAN_POINT ( 'NONE',  ( 4.158806965674306078, -4.075748668183979184, -0.05940377217583765745 ) ) ;
#19573=ORIENTED_EDGE ( 'NONE', *, *, #5351, .F. ) ;
#19610=CARTESIAN_POINT ( 'NONE',  ( 4.052424581287677796, 2.393186648133054373, -2.990837702970290835 ) ) ;
#19624=CARTESIAN_POINT ( 'NONE',  ( 0.000000000000000000, 3.031088913245528982, -1.750000000000001554 ) ) ;
#19641=FILL_AREA_STYLE_COLOUR ( '', #4853 ) ;
#19655=CARTESIAN_POINT ( 'NONE',  ( 0.02944718078674108189, -0.6813962075909465455, 3.499999999999992895 ) ) ;
#19690=CARTESIAN_POINT ( 'NONE',  ( 3.950241966887844125, -3.393956070637585309, 1.121495646998712070 ) ) ;
#19761=FILL_AREA_STYLE ('',( #19641 ) ) ;
#19807=EDGE_LOOP ( 'NONE', ( #11814, #6588, #12713 ) ) ;
#19866=ADVANCED_FACE ( 'NONE', ( #22372 ), #18966, .T. ) ;
#19877=CARTESIAN_POINT ( 'NONE',  ( 3.973110223767139626, 2.264800795684280898E-11, 3.565797985667429781 ) ) ;
#19884=COLOUR_RGB ( '', 0.72549020, 0.75294118, 0.79215686) ;
#19895=SHAPE_DEFINITION_REPRESENTATION ( #22833, #4297 ) ;
#19917=CARTESIAN_POINT ( 'NONE',  ( 4.630153689607049650, 0.000000000000000000, 0.000000000000000000 ) ) ;
#19921=CARTESIAN_POINT ( 'NONE',  ( 0.3126073911696447549, 2.020725942163688504, -3.499999999999996003 ) ) ;
#19932=ORIENTED_EDGE ( 'NONE', *, *, #6970, .F. ) ;
#19935=EDGE_CURVE ( 'NONE', #5552, #7007, #6645, .T. ) ;
#19961=CARTESIAN_POINT ( 'NONE',  ( 4.071447262713884463, -2.020725942163695166, -3.500000000000000444 ) ) ;
#19981=DIRECTION ( 'NONE',  ( -5.004010026856173173E-16, -1.201780285297635391E-31, 1.000000000000000000 ) ) ;
#19988=LINE ( 'NONE', #22105, #7063 ) ;
#20007=VERTEX_POINT ( 'NONE', #1870 ) ;
#20026=DIRECTION ( 'NONE',  ( 4.844685039213900252E-16, 1.201780285297635172E-31, -1.000000000000000000 ) ) ;
#20031=CARTESIAN_POINT ( 'NONE',  ( 0.2174200650117543709, 2.185595227304866217, -3.214438021527934453 ) ) ;
#20032=EDGE_CURVE ( 'NONE', #17450, #9641, #10817, .T. ) ;
#20034=VERTEX_POINT ( 'NONE', #14120 ) ;
#20083=CARTESIAN_POINT ( 'NONE',  ( 4.124214193018072905, -2.028338413290942555, -3.513185186763553514 ) ) ;
#20089=DIRECTION ( 'NONE',  ( -1.000000000000000000, -4.440892098500626162E-16, 5.551115123125782702E-16 ) ) ;
#20109=CARTESIAN_POINT ( 'NONE',  ( 3.366108932388589547E-15, 0.3423821193476806468, -3.500000000000009326 ) ) ;
#20112=CARTESIAN_POINT ( 'NONE',  ( 0.1388410611046139165, -3.710337782248038341, -0.5735064479039801988 ) ) ;
#20117=DIRECTION ( 'NONE',  ( 1.000000000000000000, 4.440892098500626162E-16, -5.551115123125782702E-16 ) ) ;
#20216=ORIENTED_EDGE ( 'NONE', *, *, #19558, .F. ) ;
#20243=CARTESIAN_POINT ( 'NONE',  ( 4.055492966679413058, -2.385006769472238108, -3.005124364834172113 ) ) ;
#20268=DIRECTION ( 'NONE',  ( 5.551115123125782702E-16, 1.201780285297635172E-31, -1.000000000000000000 ) ) ;
#20290=CYLINDRICAL_SURFACE ( 'NONE', #22276, 2.500000000000001332 ) ;
#20302=EDGE_LOOP ( 'NONE', ( #22032, #18794, #17425 ) ) ;
#20308=CARTESIAN_POINT ( 'NONE',  ( 0.000000000000000000, 4.041451884327383226, -1.734723475976807094E-15 ) ) ;
#20362=CARTESIAN_POINT ( 'NONE',  ( 4.093692494532772841, -2.021783646005771207, 3.501831996793841384 ) ) ;
#20389=CARTESIAN_POINT ( 'NONE',  ( 0.3126073911696447549, 2.020725942163688504, 3.499999999999997780 ) ) ;
#20481=EDGE_CURVE ( 'NONE', #6388, #7393, #18609, .T. ) ;
#20485=DIRECTION ( 'NONE',  ( 1.000000000000000000, 4.440892098500626162E-16, -5.551115123125782702E-16 ) ) ;
#20492=CARTESIAN_POINT ( 'NONE',  ( 4.165266963751726337, -2.049631966911992897, 3.550066703508902854 ) ) ;
#20502=AXIS2_PLACEMENT_3D ( 'NONE', #9769, #20842, #6246 ) ;
#20543=CARTESIAN_POINT ( 'NONE',  ( 3.951447005078447372, 3.704664227300100698, -0.5833333333333329263 ) ) ;
#20556=CARTESIAN_POINT ( 'NONE',  ( 4.158806965674306078, 1.986429158307093212, 3.559403772175838476 ) ) ;
#20592=EDGE_LOOP ( 'NONE', ( #19075, #4521, #2731, #21553 ) ) ;
#20597=ORIENTED_EDGE ( 'NONE', *, *, #4937, .F. ) ;
#20598=CIRCLE ( 'NONE', #312, 0.4999999999999978351 ) ;
#20606=CARTESIAN_POINT ( 'NONE',  ( 4.175813232069142344, -2.061359961916371830, -3.570380186727398986 ) ) ;
#20627=ORIENTED_EDGE ( 'NONE', *, *, #18691, .F. ) ;
#20649=CARTESIAN_POINT ( 'NONE',  ( 3.972073812946706806, -0.6951863858493039228, -3.565770933504609719 ) ) ;
#20659=MECHANICAL_DESIGN_GEOMETRIC_PRESENTATION_REPRESENTATION('',(#18020),#3728);
#20672=CARTESIAN_POINT ( 'NONE',  ( 4.151274195509686571, 4.079825909417490237, -1.471199427103728571E-15 ) ) ;
#20684=VERTEX_POINT ( 'NONE', #23138 ) ;
#20739=ORIENTED_EDGE ( 'NONE', *, *, #19481, .T. ) ;
#20759=CARTESIAN_POINT ( 'NONE',  ( 4.180345472528539830, 2.086001522971435040, 3.570468649087209290 ) ) ;
#20762=CARTESIAN_POINT ( 'NONE',  ( 0.000000000000000000, -3.031088913245536087, 1.750000000000003331 ) ) ;
#20763=ADVANCED_FACE ( 'NONE', ( #6259 ), #16705, .F. ) ;
#20791=FACE_OUTER_BOUND ( 'NONE', #8966, .T. ) ;
#20842=DIRECTION ( 'NONE',  ( 5.551115123125782702E-16, 2.146163712481653435E-16, -1.000000000000000000 ) ) ;
#20874=CARTESIAN_POINT ( 'NONE',  ( 4.030875481281778860, 1.403567514398415206, 3.499999999999996003 ) ) ;
#20875=DIRECTION ( 'NONE',  ( 6.938893903907224433E-16, -3.552713678800500929E-15, -1.000000000000000000 ) ) ;
#20879=CARTESIAN_POINT ( 'NONE',  ( 3.961545574370236800, 1.423222908132905307, -3.500000000000006217 ) ) ;
#20907=EDGE_LOOP ( 'NONE', ( #15448, #3685, #14832, #11314 ) ) ;
#20931=AXIS2_PLACEMENT_3D ( 'NONE', #10686, #5404, #3289 ) ;
#20960=AXIS2_PLACEMENT_3D ( 'NONE', #7964, #18553, #12915 ) ;
#20969=EDGE_LOOP ( 'NONE', ( #11880, #6945, #12355, #2751, #20216 ) ) ;
#20994=ORIENTED_EDGE ( 'NONE', *, *, #22441, .T. ) ;
#21012=CARTESIAN_POINT ( 'NONE',  ( 4.175572532730925879, 4.122058607836116551, 1.209590929910755405E-15 ) ) ;
#21023=CARTESIAN_POINT ( 'NONE',  ( 3.950241966887844569, 2.668221755853158239, 2.378504353001321903 ) ) ;
#21038=ADVANCED_FACE ( 'NONE', ( #21436 ), #21312, .F. ) ;
#21039=CARTESIAN_POINT ( 'NONE',  ( 3.951447005078449148, -2.357513599190971032, 2.916666666666663410 ) ) ;
#21082=ORIENTED_EDGE ( 'NONE', *, *, #4082, .F. ) ;
#21150=CARTESIAN_POINT ( 'NONE',  ( 4.124214193018072905, 2.028338413290942555, 3.513185186763551293 ) ) ;
#21164=CARTESIAN_POINT ( 'NONE',  ( 0.3126073911696447549, -4.041451884327383226, 0.000000000000000000 ) ) ;
#21172=CIRCLE ( 'NONE', #11008, 3.499999999999999556 ) ;
#21214=CLOSED_SHELL ( 'NONE', ( #19866, #5523, #8553, #8956, #22805, #11391, #5251, #21038, #15278, #22301, #12364, #13971, #7121, #8862, #17550, #2483, #17745, #13185, #20763, #9974, #363, #5213, #16686, #22041, #7117, #17996, #21911, #7621, #1214 ) ) ;
#21229=CARTESIAN_POINT ( 'NONE',  ( 3.878089031707361301, 0.7015470581927649718, 3.499999999999996003 ) ) ;
#21244=ORIENTED_EDGE ( 'NONE', *, *, #22967, .F. ) ;
#21265=ORIENTED_EDGE ( 'NONE', *, *, #2753, .F. ) ;
#21270=CARTESIAN_POINT ( 'NONE',  ( 4.071447262713884463, 2.020725942163688504, -3.499999999999999556 ) ) ;
#21305=CARTESIAN_POINT ( 'NONE',  ( 0.1397371499203187151, 1.362866705341262197, -3.500000000000009770 ) ) ;
#21312=PLANE ( 'NONE',  #11515 ) ;
#21398=CARTESIAN_POINT ( 'NONE',  ( 3.950241966888151435, 3.393956070637460520, -1.121495646999018270 ) ) ;
#21399=CARTESIAN_POINT ( 'NONE',  ( 4.170895651974849905, -2.054890354522451279, -3.559174498016467680 ) ) ;
#21436=FACE_OUTER_BOUND ( 'NONE', #17871, .T. ) ;
#21478=DIRECTION ( 'NONE',  ( -1.000000000000000000, -4.440892098500626162E-16, 5.551115123125782702E-16 ) ) ;
#21553=ORIENTED_EDGE ( 'NONE', *, *, #4713, .F. ) ;
#21655=CARTESIAN_POINT ( 'NONE',  ( 0.000000000000000000, 0.000000000000000000, -3.499999999999996003 ) ) ;
#21700=CARTESIAN_POINT ( 'NONE',  ( 4.158413352280801334, 2.044871626972824430, 3.541821552872959966 ) ) ;
#21710=DIRECTION ( 'NONE',  ( -1.000000000000000000, -4.440892098500626162E-16, 5.551115123125782702E-16 ) ) ;
#21732=CARTESIAN_POINT ( 'NONE',  ( 4.175813232069142344, 2.061359961916371830, 3.570380186727395433 ) ) ;
#21773=CARTESIAN_POINT ( 'NONE',  ( 3.951447005078449148, -1.347150628109124559, -3.500000000000001332 ) ) ;
#21817=ORIENTED_EDGE ( 'NONE', *, *, #5351, .T. ) ;
#21818=ORIENTED_EDGE ( 'NONE', *, *, #14570, .F. ) ;
#21836=B_SPLINE_CURVE_WITH_KNOTS ( 'NONE', 3,
 ( #7528, #21996, #14690, #20112, #9522, #16678 ),
 .UNSPECIFIED., .F., .F.,
 ( 4, 2, 4 ),
 ( 0.002044882221487528875, 0.003063384235218492846, 0.004081886248949457251 ),
 .UNSPECIFIED. ) ;
#21843=CARTESIAN_POINT ( 'NONE',  ( 4.165266963751727225, -2.049631966911992897, -3.550066703508901078 ) ) ;
#21853=PRODUCT_DEFINITION ( 'UNKNOWN', '', #759, #2056 ) ;
#21881=CARTESIAN_POINT ( 'NONE',  ( 4.175572532730925879, 2.061029303918053390, -3.569807470274388717 ) ) ;
#21911=ADVANCED_FACE ( 'NONE', ( #13582 ), #7607, .F. ) ;
#21996=CARTESIAN_POINT ( 'NONE',  ( 2.954027403549371644E-15, -3.202582148906737647, -1.452965002680429052 ) ) ;
#22004=ORIENTED_EDGE ( 'NONE', *, *, #16197, .F. ) ;
#22032=ORIENTED_EDGE ( 'NONE', *, *, #22468, .T. ) ;
#22041=ADVANCED_FACE ( 'NONE', ( #12496 ), #14646, .F. ) ;
#22042=CARTESIAN_POINT ( 'NONE',  ( 0.000000000000000000, -3.031088913245536087, 1.750000000000003331 ) ) ;
#22043=EDGE_CURVE ( 'NONE', #10215, #4400, #17448, .T. ) ;
#22044=CARTESIAN_POINT ( 'NONE',  ( 3.853576393533437815E-15, -0.3420925509381499419, -3.500000000000009770 ) ) ;
#22056=EDGE_CURVE ( 'NONE', #5230, #7393, #22151, .T. ) ;
#22093=AXIS2_PLACEMENT_3D ( 'NONE', #9703, #6057, #13226 ) ;
#22105=CARTESIAN_POINT ( 'NONE',  ( 5.599999999999994316, -4.041451884327383226, 0.000000000000000000 ) ) ;
#22115=AXIS2_PLACEMENT_3D ( 'NONE', #4943, #2963, #5306 ) ;
#22151=B_SPLINE_CURVE_WITH_KNOTS ( 'NONE', 3,
 ( #3790, #7450, #5811, #54 ),
 .UNSPECIFIED., .F., .F.,
 ( 4, 4 ),
 ( 2.380739282183830354E-07, 0.002044882221487538416 ),
 .UNSPECIFIED. ) ;
#22156=VERTEX_POINT ( 'NONE', #22381 ) ;
#22169=DIRECTION ( 'NONE',  ( 7.027852765209223361E-16, 0.5000000000000009992, -0.8660254037844381525 ) ) ;
#22171=FACE_BOUND ( 'NONE', #8038, .T. ) ;
#22205=CARTESIAN_POINT ( 'NONE',  ( 0.2182387239012628377, 1.693823289460905768, 3.499999999999994227 ) ) ;
#22221=B_SPLINE_CURVE_WITH_KNOTS ( 'NONE', 3,
 ( #18773, #20543, #4646, #22536, #1012 ),
 .UNSPECIFIED., .F., .F.,
 ( 4, 1, 4 ),
 ( 0.000000000000000000, 0.002020725942163691374, 0.004041451884327382747 ),
 .UNSPECIFIED. ) ;
#22229=CARTESIAN_POINT ( 'NONE',  ( 4.071447262713884463, 2.020725942163688504, -3.499999999999999556 ) ) ;
#22231=CARTESIAN_POINT ( 'NONE',  ( 4.082498951862916670, 2.020725942163687616, -3.500000000000001332 ) ) ;
#22245=CARTESIAN_POINT ( 'NONE',  ( 4.124214193018073793, -2.028338413290942110, 3.513185186763553958 ) ) ;
#22254=CARTESIAN_POINT ( 'NONE',  ( 3.973110223768741456, 0.6864646529411790876, 3.565797985667471970 ) ) ;
#22276=AXIS2_PLACEMENT_3D ( 'NONE', #11100, #21710, #2399 ) ;
#22282=DIRECTION ( 'NONE',  ( -1.000000000000000000, -4.440892098500626162E-16, 5.551115123125782702E-16 ) ) ;
#22301=ADVANCED_FACE ( 'NONE', ( #3405 ), #10787, .T. ) ;
#22344=DIRECTION ( 'NONE',  ( -1.000000000000000000, -4.440892098500626162E-16, 5.551115123125782702E-16 ) ) ;
#22357=ORIENTED_EDGE ( 'NONE', *, *, #16566, .T. ) ;
#22370=CARTESIAN_POINT ( 'NONE',  ( 4.175813232069142344, -2.061359961916364725, 3.570380186727395433 ) ) ;
#22371=CARTESIAN_POINT ( 'NONE',  ( 4.050536630291683871, -3.778525289263160225, -0.5912575323401451088 ) ) ;
#22372=FACE_OUTER_BOUND ( 'NONE', #4843, .T. ) ;
#22381=CARTESIAN_POINT ( 'NONE',  ( 4.175813232069142344, 2.061359961916364725, -3.570380186727397209 ) ) ;
#22385=ORIENTED_EDGE ( 'NONE', *, *, #19481, .F. ) ;
#22395=CARTESIAN_POINT ( 'NONE',  ( 0.000000000000000000, 0.000000000000000000, 0.000000000000000000 ) ) ;
#22424=CARTESIAN_POINT ( 'NONE',  ( 4.082498951862915781, 4.041451884327383226, -6.134919877127760970E-18 ) ) ;
#22440=B_SPLINE_CURVE_WITH_KNOTS ( 'NONE', 3,
 ( #1651, #5178, #3306, #1984, #9050 ),
 .UNSPECIFIED., .F., .F.,
 ( 4, 1, 4 ),
 ( 0.000000000000000000, 0.002020725942163690073, 0.004041451884327380145 ),
 .UNSPECIFIED. ) ;
#22441=EDGE_CURVE ( 'NONE', #3580, #4523, #9389, .T. ) ;
#22460=CARTESIAN_POINT ( 'NONE',  ( 0.000000000000000000, -3.031088913245536087, 1.750000000000003331 ) ) ;
#22468=EDGE_CURVE ( 'NONE', #14654, #6, #17342, .T. ) ;
#22476=CIRCLE ( 'NONE', #12318, 2.500000000000002220 ) ;
#22479=EDGE_CURVE ( 'NONE', #4649, #17450, #17176, .T. ) ;
#22504=EDGE_LOOP ( 'NONE', ( #10345, #20994, #16871, #10967, #17004, #16443, #2999 ) ) ;
#22536=CARTESIAN_POINT ( 'NONE',  ( 3.951447005078449148, 2.357513599190971920, -2.916666666666667407 ) ) ;
#22544=DIRECTION ( 'NONE',  ( -4.440892098500625669E-16, 1.000000000000000000, 1.224646799147351975E-16 ) ) ;
#22579=ORIENTED_EDGE ( 'NONE', *, *, #10023, .T. ) ;
#22583=ORIENTED_EDGE ( 'NONE', *, *, #9360, .F. ) ;
#22614=ORIENTED_EDGE ( 'NONE', *, *, #3490, .F. ) ;
#22654=LINE ( 'NONE', #18774, #7238 ) ;
#22745=CARTESIAN_POINT ( 'NONE',  ( 3.951447005078450037, 1.347150628109125670, 3.499999999999999112 ) ) ;
#22799=DIRECTION ( 'NONE',  ( 0.000000000000000000, 0.000000000000000000, 1.000000000000000000 ) ) ;
#22805=ADVANCED_FACE ( 'NONE', ( #22171, #2870 ), #10047, .T. ) ;
#22833=PRODUCT_DEFINITION_SHAPE ( 'NONE', 'NONE',  #21853 ) ;
#22915=EDGE_LOOP ( 'NONE', ( #17966, #19338, #933 ) ) ;
#22929=DIRECTION ( 'NONE',  ( 1.000000000000000000, 4.440892098500626162E-16, -5.551115123125782702E-16 ) ) ;
#22967=EDGE_CURVE ( 'NONE', #7393, #19198, #9479, .T. ) ;
#23022=EDGE_CURVE ( 'NONE', #7393, #12162, #12682, .T. ) ;
#23033=B_SPLINE_CURVE_WITH_KNOTS ( 'NONE', 3,
 ( #15202, #22044, #15320, #527, #18626, #14975 ),
 .UNSPECIFIED., .F., .F.,
 ( 4, 2, 4 ),
 ( 0.01308430721348209647, 0.01410661710602281738, 0.01512892699856353829 ),
 .UNSPECIFIED. ) ;
#23122=ORIENTED_EDGE ( 'NONE', *, *, #6032, .F. ) ;
#23138=CARTESIAN_POINT ( 'NONE',  ( 4.071447262713884463, -2.020725942163695166, -3.500000000000000444 ) ) ;
#23143=SHAPE_REPRESENTATION_RELATIONSHIP ( 'NONE' , 'NONE' ,  #4297, #19561 ) ;
#23158=CARTESIAN_POINT ( 'NONE',  ( 4.158806965674305189, 4.075748668183988066, 0.05940377217583944769 ) ) ;
#23177=CARTESIAN_POINT ( 'NONE',  ( 0.000000000000000000, -3.031088913245536087, -1.749999999999996447 ) ) ;
#23198=B_SPLINE_CURVE_WITH_KNOTS ( 'NONE', 3,
 ( #14615, #3901, #2023, #13081, #5808, #505 ),
 .UNSPECIFIED., .F., .F.,
 ( 4, 2, 4 ),
 ( 0.000000000000000000, 0.002086519881787257148, 0.004173039763574514296 ),
 .UNSPECIFIED. ) ;
#23233=CARTESIAN_POINT ( 'NONE',  ( 4.033901012035799205, -3.740908793663177523, 0.5205559028926609599 ) ) ;
#23239=EDGE_CURVE ( 'NONE', #2560, #3580, #10851, .T. ) ;
#23246=DIRECTION ( 'NONE',  ( -5.004010026856173173E-16, -1.201780285297635391E-31, 1.000000000000000000 ) ) ;
ENDSEC;
END-ISO-10303-21;
